ISO-10303-21;
HEADER;
/* Generated by software containing ST-Developer
 * from STEP Tools, Inc. (www.steptools.com) 
 */

FILE_DESCRIPTION(
/* description */ (''),
/* implementation_level */ '2;1');

FILE_NAME(
/* name */ 'ISO 4026 - M3 x 3 - 45H (Knob Set Screw).step',
/* time_stamp */ '2026-10-05T09:57:53+05:00',
/* author */ (''),
/* organization */ (''),
/* preprocessor_version */ 'ST-DEVELOPER v20.2',
/* originating_system */ 'Autodesk Translation Framework v15.15.0.0',
/* authorisation */ '');

FILE_SCHEMA (('AUTOMOTIVE_DESIGN { 1 0 10303 214 3 1 1 }'));
ENDSEC;

DATA;
#10=MECHANICAL_DESIGN_GEOMETRIC_PRESENTATION_REPRESENTATION('',(#562),#113984);
#383=(
BOUNDED_CURVE()
B_SPLINE_CURVE(2,(#105405,#105406,#105407),.UNSPECIFIED.,.F.,.F.)
B_SPLINE_CURVE_WITH_KNOTS((3,3),(0.,0.0136874154102675),.UNSPECIFIED.)
CURVE()
GEOMETRIC_REPRESENTATION_ITEM()
RATIONAL_B_SPLINE_CURVE((1.,1.00669106236177,1.00897713804878))
REPRESENTATION_ITEM('')
);
#384=(
BOUNDED_CURVE()
B_SPLINE_CURVE(2,(#105411,#105412,#105413),.UNSPECIFIED.,.F.,.F.)
B_SPLINE_CURVE_WITH_KNOTS((3,3),(0.0278942541126669,0.0415816695229366),
 .UNSPECIFIED.)
CURVE()
GEOMETRIC_REPRESENTATION_ITEM()
RATIONAL_B_SPLINE_CURVE((1.0089771380491,1.00669106236202,1.))
REPRESENTATION_ITEM('')
);
#385=(
BOUNDED_CURVE()
B_SPLINE_CURVE(2,(#105415,#105416,#105417),.UNSPECIFIED.,.F.,.F.)
B_SPLINE_CURVE_WITH_KNOTS((3,3),(0.,0.013687415410265),.UNSPECIFIED.)
CURVE()
GEOMETRIC_REPRESENTATION_ITEM()
RATIONAL_B_SPLINE_CURVE((1.,1.00669106236252,1.00897713804979))
REPRESENTATION_ITEM('')
);
#386=(
BOUNDED_CURVE()
B_SPLINE_CURVE(2,(#105421,#105422,#105423),.UNSPECIFIED.,.F.,.F.)
B_SPLINE_CURVE_WITH_KNOTS((3,3),(0.02789425411267,0.041581669522935),
 .UNSPECIFIED.)
CURVE()
GEOMETRIC_REPRESENTATION_ITEM()
RATIONAL_B_SPLINE_CURVE((1.00897713804979,1.00669106236252,1.))
REPRESENTATION_ITEM('')
);
#387=(
BOUNDED_CURVE()
B_SPLINE_CURVE(2,(#105425,#105426,#105427),.UNSPECIFIED.,.F.,.F.)
B_SPLINE_CURVE_WITH_KNOTS((3,3),(0.,0.0136874154102697),.UNSPECIFIED.)
CURVE()
GEOMETRIC_REPRESENTATION_ITEM()
RATIONAL_B_SPLINE_CURVE((1.,1.00669106236202,1.0089771380491))
REPRESENTATION_ITEM('')
);
#388=(
BOUNDED_CURVE()
B_SPLINE_CURVE(2,(#105431,#105432,#105433),.UNSPECIFIED.,.F.,.F.)
B_SPLINE_CURVE_WITH_KNOTS((3,3),(0.0278942541126704,0.0415816695229368),
 .UNSPECIFIED.)
CURVE()
GEOMETRIC_REPRESENTATION_ITEM()
RATIONAL_B_SPLINE_CURVE((1.00897713804836,1.00669106236146,1.))
REPRESENTATION_ITEM('')
);
#389=(
BOUNDED_CURVE()
B_SPLINE_CURVE(2,(#105435,#105436,#105437),.UNSPECIFIED.,.F.,.F.)
B_SPLINE_CURVE_WITH_KNOTS((3,3),(0.,0.0136874154102591),.UNSPECIFIED.)
CURVE()
GEOMETRIC_REPRESENTATION_ITEM()
RATIONAL_B_SPLINE_CURVE((1.,1.00669106236259,1.00897713804988))
REPRESENTATION_ITEM('')
);
#390=(
BOUNDED_CURVE()
B_SPLINE_CURVE(2,(#105441,#105442,#105443),.UNSPECIFIED.,.F.,.F.)
B_SPLINE_CURVE_WITH_KNOTS((3,3),(0.0278942541126758,0.0415816695229351),
 .UNSPECIFIED.)
CURVE()
GEOMETRIC_REPRESENTATION_ITEM()
RATIONAL_B_SPLINE_CURVE((1.00897713804987,1.00669106236259,1.))
REPRESENTATION_ITEM('')
);
#391=(
BOUNDED_CURVE()
B_SPLINE_CURVE(2,(#105445,#105446,#105447),.UNSPECIFIED.,.F.,.F.)
B_SPLINE_CURVE_WITH_KNOTS((3,3),(0.,0.0136874154102569),.UNSPECIFIED.)
CURVE()
GEOMETRIC_REPRESENTATION_ITEM()
RATIONAL_B_SPLINE_CURVE((1.,1.00669106236306,1.0089771380505))
REPRESENTATION_ITEM('')
);
#392=(
BOUNDED_CURVE()
B_SPLINE_CURVE(2,(#105451,#105452,#105453),.UNSPECIFIED.,.F.,.F.)
B_SPLINE_CURVE_WITH_KNOTS((3,3),(0.0278942541126783,0.0415816695229351),
 .UNSPECIFIED.)
CURVE()
GEOMETRIC_REPRESENTATION_ITEM()
RATIONAL_B_SPLINE_CURVE((1.0089771380505,1.00669106236306,1.))
REPRESENTATION_ITEM('')
);
#393=(
BOUNDED_CURVE()
B_SPLINE_CURVE(2,(#105455,#105456,#105457),.UNSPECIFIED.,.F.,.F.)
B_SPLINE_CURVE_WITH_KNOTS((3,3),(0.,0.0136874154102613),.UNSPECIFIED.)
CURVE()
GEOMETRIC_REPRESENTATION_ITEM()
RATIONAL_B_SPLINE_CURVE((1.,1.00669106236177,1.00897713804878))
REPRESENTATION_ITEM('')
);
#394=(
BOUNDED_CURVE()
B_SPLINE_CURVE(2,(#105460,#105461,#105462),.UNSPECIFIED.,.F.,.F.)
B_SPLINE_CURVE_WITH_KNOTS((3,3),(0.027894254112673,0.0415816695229326),
 .UNSPECIFIED.)
CURVE()
GEOMETRIC_REPRESENTATION_ITEM()
RATIONAL_B_SPLINE_CURVE((1.00897713804929,1.00669106236215,1.))
REPRESENTATION_ITEM('')
);
#526=SHAPE_REPRESENTATION_RELATIONSHIP('SRR','None',#114063,#544);
#544=ADVANCED_BREP_SHAPE_REPRESENTATION('',(#580),#113977);
#562=STYLED_ITEM('',(#114317),#580);
#580=MANIFOLD_SOLID_BREP('ISO 4026 - M3 x 3 - 45H (Knob Set Screw)',#60403);
#742=CYLINDRICAL_SURFACE('',#63116,1.4635);
#743=CYLINDRICAL_SURFACE('',#63118,1.4635);
#744=CYLINDRICAL_SURFACE('',#63119,1.4635);
#745=CYLINDRICAL_SURFACE('',#63120,1.4635);
#746=CYLINDRICAL_SURFACE('',#63121,1.4635);
#747=CYLINDRICAL_SURFACE('',#63122,1.17775);
#748=CYLINDRICAL_SURFACE('',#63124,1.17775);
#749=CYLINDRICAL_SURFACE('',#63125,1.17775);
#750=CYLINDRICAL_SURFACE('',#63126,1.17775);
#751=CYLINDRICAL_SURFACE('',#63134,1.17775);
#752=CYLINDRICAL_SURFACE('',#63143,0.816025403784444);
#753=CYLINDRICAL_SURFACE('',#63145,0.816025403784444);
#754=CYLINDRICAL_SURFACE('',#63147,0.816025403784444);
#755=CYLINDRICAL_SURFACE('',#63149,0.816025403784444);
#756=CYLINDRICAL_SURFACE('',#63151,0.816025403784444);
#757=CYLINDRICAL_SURFACE('',#63153,0.816025403784444);
#758=CYLINDRICAL_SURFACE('',#63183,1.4635);
#933=CONICAL_SURFACE('',#63135,0.916025403784442,0.785398163397437);
#934=CONICAL_SURFACE('',#63176,0.866025403784434,1.02974425867665);
#935=CONICAL_SURFACE('',#63182,1.35000000000002,0.785398163397434);
#936=CONICAL_SURFACE('',#63185,1.25,0.785398163397457);
#1303=CIRCLE('',#63117,1.4635);
#1304=CIRCLE('',#63123,1.17775);
#1305=CIRCLE('',#63128,1.4635);
#1306=CIRCLE('',#63129,1.4635);
#1307=CIRCLE('',#63131,1.4635);
#1308=CIRCLE('',#63132,1.4635);
#1309=CIRCLE('',#63133,1.17775);
#1310=CIRCLE('',#63136,1.01602540378444);
#1311=CIRCLE('',#63137,0.816025403784444);
#1312=CIRCLE('',#63138,0.816025403784444);
#1313=CIRCLE('',#63139,0.816025403784444);
#1314=CIRCLE('',#63140,0.816025403784444);
#1315=CIRCLE('',#63141,0.816025403784444);
#1316=CIRCLE('',#63142,0.816025403784444);
#1317=CIRCLE('',#63144,0.816025403784444);
#1318=CIRCLE('',#63146,0.816025403784444);
#1319=CIRCLE('',#63148,0.816025403784444);
#1320=CIRCLE('',#63150,0.816025403784444);
#1321=CIRCLE('',#63152,0.816025403784444);
#1322=CIRCLE('',#63154,0.816025403784444);
#1323=CIRCLE('',#63165,0.866025403784434);
#1324=CIRCLE('',#63167,0.866025403784434);
#1325=CIRCLE('',#63169,0.866025403784434);
#1326=CIRCLE('',#63171,0.866025403784434);
#1327=CIRCLE('',#63173,0.866025403784434);
#1328=CIRCLE('',#63175,0.866025403784434);
#1329=CIRCLE('',#63181,1.20000000000001);
#1330=CIRCLE('',#63184,1.4635);
#1331=CIRCLE('',#63186,0.999999999999996);
#1852=FACE_BOUND('',#10507,.T.);
#3793=PLANE('',#63127);
#3794=PLANE('',#63130);
#3795=PLANE('',#63155);
#3796=PLANE('',#63156);
#3797=PLANE('',#63157);
#3798=PLANE('',#63158);
#3799=PLANE('',#63159);
#3800=PLANE('',#63160);
#3801=PLANE('',#63161);
#3802=PLANE('',#63162);
#3803=PLANE('',#63163);
#3804=PLANE('',#63164);
#3805=PLANE('',#63166);
#3806=PLANE('',#63168);
#3807=PLANE('',#63170);
#3808=PLANE('',#63172);
#3809=PLANE('',#63174);
#3810=PLANE('',#63177);
#3811=PLANE('',#63178);
#3812=PLANE('',#63179);
#3813=PLANE('',#63180);
#3814=PLANE('',#63187);
#6889=FACE_OUTER_BOUND('',#10466,.T.);
#6890=FACE_OUTER_BOUND('',#10467,.T.);
#6891=FACE_OUTER_BOUND('',#10468,.T.);
#6892=FACE_OUTER_BOUND('',#10469,.T.);
#6893=FACE_OUTER_BOUND('',#10470,.T.);
#6894=FACE_OUTER_BOUND('',#10471,.T.);
#6895=FACE_OUTER_BOUND('',#10472,.T.);
#6896=FACE_OUTER_BOUND('',#10473,.T.);
#6897=FACE_OUTER_BOUND('',#10474,.T.);
#6898=FACE_OUTER_BOUND('',#10475,.T.);
#6899=FACE_OUTER_BOUND('',#10476,.T.);
#6900=FACE_OUTER_BOUND('',#10477,.T.);
#6901=FACE_OUTER_BOUND('',#10478,.T.);
#6902=FACE_OUTER_BOUND('',#10479,.T.);
#6903=FACE_OUTER_BOUND('',#10480,.T.);
#6904=FACE_OUTER_BOUND('',#10481,.T.);
#6905=FACE_OUTER_BOUND('',#10482,.T.);
#6906=FACE_OUTER_BOUND('',#10483,.T.);
#6907=FACE_OUTER_BOUND('',#10484,.T.);
#6908=FACE_OUTER_BOUND('',#10485,.T.);
#6909=FACE_OUTER_BOUND('',#10486,.T.);
#6910=FACE_OUTER_BOUND('',#10487,.T.);
#6911=FACE_OUTER_BOUND('',#10488,.T.);
#6912=FACE_OUTER_BOUND('',#10489,.T.);
#6913=FACE_OUTER_BOUND('',#10490,.T.);
#6914=FACE_OUTER_BOUND('',#10491,.T.);
#6915=FACE_OUTER_BOUND('',#10492,.T.);
#6916=FACE_OUTER_BOUND('',#10493,.T.);
#6917=FACE_OUTER_BOUND('',#10494,.T.);
#6918=FACE_OUTER_BOUND('',#10495,.T.);
#6919=FACE_OUTER_BOUND('',#10496,.T.);
#6920=FACE_OUTER_BOUND('',#10497,.T.);
#6921=FACE_OUTER_BOUND('',#10498,.T.);
#6922=FACE_OUTER_BOUND('',#10499,.T.);
#6923=FACE_OUTER_BOUND('',#10500,.T.);
#6924=FACE_OUTER_BOUND('',#10501,.T.);
#6925=FACE_OUTER_BOUND('',#10502,.T.);
#6926=FACE_OUTER_BOUND('',#10503,.T.);
#6927=FACE_OUTER_BOUND('',#10504,.T.);
#6928=FACE_OUTER_BOUND('',#10505,.T.);
#6929=FACE_OUTER_BOUND('',#10506,.T.);
#6930=FACE_OUTER_BOUND('',#10508,.T.);
#6931=FACE_OUTER_BOUND('',#10509,.T.);
#6932=FACE_OUTER_BOUND('',#10510,.T.);
#6933=FACE_OUTER_BOUND('',#10511,.T.);
#10466=EDGE_LOOP('',(#54299,#54300,#54301,#54302));
#10467=EDGE_LOOP('',(#54303,#54304,#54305,#54306));
#10468=EDGE_LOOP('',(#54307,#54308,#54309,#54310));
#10469=EDGE_LOOP('',(#54311,#54312,#54313,#54314));
#10470=EDGE_LOOP('',(#54315,#54316,#54317,#54318));
#10471=EDGE_LOOP('',(#54319,#54320,#54321,#54322));
#10472=EDGE_LOOP('',(#54323,#54324,#54325,#54326));
#10473=EDGE_LOOP('',(#54327,#54328,#54329,#54330));
#10474=EDGE_LOOP('',(#54331,#54332,#54333,#54334));
#10475=EDGE_LOOP('',(#54335,#54336,#54337,#54338,#54339));
#10476=EDGE_LOOP('',(#54340,#54341,#54342,#54343,#54344,#54345,#54346,#54347,
#54348,#54349,#54350,#54351,#54352));
#10477=EDGE_LOOP('',(#54353,#54354,#54355,#54356,#54357));
#10478=EDGE_LOOP('',(#54358,#54359,#54360,#54361));
#10479=EDGE_LOOP('',(#54362,#54363,#54364,#54365,#54366,#54367,#54368,#54369,
#54370,#54371,#54372,#54373,#54374));
#10480=EDGE_LOOP('',(#54375,#54376,#54377,#54378,#54379,#54380,#54381,#54382,
#54383,#54384,#54385,#54386,#54387,#54388,#54389,#54390,#54391,#54392,#54393,
#54394,#54395));
#10481=EDGE_LOOP('',(#54396,#54397,#54398,#54399));
#10482=EDGE_LOOP('',(#54400,#54401,#54402,#54403));
#10483=EDGE_LOOP('',(#54404,#54405,#54406,#54407));
#10484=EDGE_LOOP('',(#54408,#54409,#54410,#54411));
#10485=EDGE_LOOP('',(#54412,#54413,#54414,#54415));
#10486=EDGE_LOOP('',(#54416,#54417,#54418,#54419));
#10487=EDGE_LOOP('',(#54420,#54421,#54422,#54423,#54424,#54425,#54426,#54427));
#10488=EDGE_LOOP('',(#54428,#54429,#54430,#54431,#54432,#54433,#54434,#54435));
#10489=EDGE_LOOP('',(#54436,#54437,#54438,#54439,#54440,#54441,#54442,#54443));
#10490=EDGE_LOOP('',(#54444,#54445));
#10491=EDGE_LOOP('',(#54446,#54447));
#10492=EDGE_LOOP('',(#54448,#54449));
#10493=EDGE_LOOP('',(#54450,#54451));
#10494=EDGE_LOOP('',(#54452,#54453));
#10495=EDGE_LOOP('',(#54454,#54455));
#10496=EDGE_LOOP('',(#54456,#54457));
#10497=EDGE_LOOP('',(#54458,#54459));
#10498=EDGE_LOOP('',(#54460,#54461));
#10499=EDGE_LOOP('',(#54462,#54463));
#10500=EDGE_LOOP('',(#54464,#54465));
#10501=EDGE_LOOP('',(#54466,#54467));
#10502=EDGE_LOOP('',(#54468,#54469,#54470,#54471,#54472,#54473,#54474,#54475));
#10503=EDGE_LOOP('',(#54476,#54477,#54478,#54479,#54480,#54481,#54482,#54483));
#10504=EDGE_LOOP('',(#54484,#54485,#54486,#54487,#54488,#54489,#54490,#54491));
#10505=EDGE_LOOP('',(#54492,#54493,#54494,#54495,#54496,#54497,#54498,#54499));
#10506=EDGE_LOOP('',(#54500));
#10507=EDGE_LOOP('',(#54501));
#10508=EDGE_LOOP('',(#54502,#54503,#54504,#54505,#54506,#54507));
#10509=EDGE_LOOP('',(#54508,#54509,#54510,#54511));
#10510=EDGE_LOOP('',(#54512,#54513,#54514,#54515,#54516,#54517));
#10511=EDGE_LOOP('',(#54518));
#16447=LINE('',#104428,#22481);
#16448=LINE('',#104452,#22482);
#16449=LINE('',#104500,#22483);
#16450=LINE('',#104548,#22484);
#16451=LINE('',#104602,#22485);
#16452=LINE('',#104650,#22486);
#16453=LINE('',#104674,#22487);
#16454=LINE('',#104699,#22488);
#16455=LINE('',#104724,#22489);
#16456=LINE('',#105403,#22490);
#16457=LINE('',#105465,#22491);
#16458=LINE('',#105467,#22492);
#16459=LINE('',#105471,#22493);
#16460=LINE('',#105473,#22494);
#16461=LINE('',#105477,#22495);
#16462=LINE('',#105480,#22496);
#16463=LINE('',#105483,#22497);
#16464=LINE('',#105485,#22498);
#16465=LINE('',#105489,#22499);
#16466=LINE('',#105492,#22500);
#16467=LINE('',#105495,#22501);
#16468=LINE('',#105498,#22502);
#16469=LINE('',#105500,#22503);
#16470=LINE('',#105502,#22504);
#16471=LINE('',#105504,#22505);
#16472=LINE('',#105505,#22506);
#16473=LINE('',#105507,#22507);
#16474=LINE('',#105509,#22508);
#16475=LINE('',#105510,#22509);
#16476=LINE('',#105512,#22510);
#16477=LINE('',#105514,#22511);
#16478=LINE('',#105515,#22512);
#16479=LINE('',#105519,#22513);
#16480=LINE('',#105522,#22514);
#16481=LINE('',#105524,#22515);
#16482=LINE('',#105527,#22516);
#16483=LINE('',#105537,#22517);
#16484=LINE('',#105540,#22518);
#16485=LINE('',#105544,#22519);
#16486=LINE('',#105546,#22520);
#16487=LINE('',#105548,#22521);
#16488=LINE('',#105554,#22522);
#16489=LINE('',#105560,#22523);
#22481=VECTOR('',#74363,1.5);
#22482=VECTOR('',#74368,1.5);
#22483=VECTOR('',#74371,1.5);
#22484=VECTOR('',#74374,1.5);
#22485=VECTOR('',#74377,1.5);
#22486=VECTOR('',#74380,1.17775);
#22487=VECTOR('',#74385,1.17775);
#22488=VECTOR('',#74388,1.17775);
#22489=VECTOR('',#74391,1.17775);
#22490=VECTOR('',#74412,0.916025403784442);
#22491=VECTOR('',#74427,10.);
#22492=VECTOR('',#74428,10.);
#22493=VECTOR('',#74433,10.);
#22494=VECTOR('',#74434,10.);
#22495=VECTOR('',#74439,10.);
#22496=VECTOR('',#74442,10.);
#22497=VECTOR('',#74445,10.);
#22498=VECTOR('',#74446,10.);
#22499=VECTOR('',#74451,10.);
#22500=VECTOR('',#74454,10.);
#22501=VECTOR('',#74457,10.);
#22502=VECTOR('',#74460,10.);
#22503=VECTOR('',#74463,10.);
#22504=VECTOR('',#74464,10.);
#22505=VECTOR('',#74465,10.);
#22506=VECTOR('',#74466,10.);
#22507=VECTOR('',#74469,10.);
#22508=VECTOR('',#74470,10.);
#22509=VECTOR('',#74471,10.);
#22510=VECTOR('',#74474,10.);
#22511=VECTOR('',#74475,10.);
#22512=VECTOR('',#74476,10.);
#22513=VECTOR('',#74483,10.);
#22514=VECTOR('',#74488,10.);
#22515=VECTOR('',#74491,10.);
#22516=VECTOR('',#74494,10.);
#22517=VECTOR('',#74511,10.);
#22518=VECTOR('',#74516,10.);
#22519=VECTOR('',#74521,0.866025403784434);
#22520=VECTOR('',#74524,10.);
#22521=VECTOR('',#74527,10.);
#22522=VECTOR('',#74536,1.35000000000002);
#22523=VECTOR('',#74545,1.25);
#24400=B_SPLINE_CURVE_WITH_KNOTS('',3,(#104430,#104431,#104432,#104433,
#104434,#104435,#104436,#104437,#104438,#104439),.UNSPECIFIED.,.F.,.F.,
(4,3,3,4),(-4.09202352044854,-3.95310104254947,-2.9648257819121,-2.07317267331967),
 .UNSPECIFIED.);
#24401=B_SPLINE_CURVE_WITH_KNOTS('',3,(#104442,#104443,#104444,#104445,
#104446,#104447,#104448),.UNSPECIFIED.,.F.,.F.,(4,3,4),(0.,0.988275260637351,
1.12274180646091),.UNSPECIFIED.);
#24402=B_SPLINE_CURVE_WITH_KNOTS('',3,(#104453,#104454,#104455,#104456,
#104457,#104458,#104459,#104460,#104461,#104462,#104463,#104464,#104465,
#104466,#104467,#104468,#104469,#104470,#104471,#104472,#104473,#104474),
 .UNSPECIFIED.,.F.,.F.,(4,3,3,3,3,3,3,4),(-10.3752088276281,-9.88275260637366,
-8.8944773457363,-7.90620208509893,-6.91792682446157,-5.9296515638242,-4.94137630318683,
-4.09202352044854),.UNSPECIFIED.);
#24403=B_SPLINE_CURVE_WITH_KNOTS('',3,(#104475,#104476,#104477,#104478,
#104479,#104480,#104481,#104482,#104483,#104484,#104485,#104486,#104487,
#104488,#104489,#104490,#104491,#104492,#104493,#104494,#104495,#104496),
 .UNSPECIFIED.,.F.,.F.,(4,3,3,3,3,3,3,4),(1.12274180646091,1.97655052127471,
2.96482578191208,3.95310104254944,4.94137630318681,5.92965156382417,6.91792682446154,
7.40592711364053),.UNSPECIFIED.);
#24404=B_SPLINE_CURVE_WITH_KNOTS('',3,(#104501,#104502,#104503,#104504,
#104505,#104506,#104507,#104508,#104509,#104510,#104511,#104512,#104513,
#104514,#104515,#104516,#104517,#104518,#104519,#104520,#104521,#104522),
 .UNSPECIFIED.,.F.,.F.,(4,3,3,3,3,3,3,4),(-16.6583941348077,-15.8124041701979,
-14.8241289095605,-13.8358536489231,-12.8475783882858,-11.8593031276484,
-10.871027867011,-10.3752088276281),.UNSPECIFIED.);
#24405=B_SPLINE_CURVE_WITH_KNOTS('',3,(#104523,#104524,#104525,#104526,
#104527,#104528,#104529,#104530,#104531,#104532,#104533,#104534,#104535,
#104536,#104537,#104538,#104539,#104540,#104541,#104542,#104543,#104544),
 .UNSPECIFIED.,.F.,.F.,(4,3,3,3,3,3,3,4),(7.40592711364053,7.9062020850989,
8.89447734573626,9.88275260637363,10.871027867011,11.8593031276484,12.8475783882857,
13.6891124208201),.UNSPECIFIED.);
#24406=B_SPLINE_CURVE_WITH_KNOTS('',3,(#104549,#104550,#104551,#104552,
#104553,#104554,#104555,#104556,#104557,#104558,#104559,#104560,#104561,
#104562,#104563,#104564,#104565,#104566,#104567,#104568,#104569,#104570,
#104571,#104572,#104573),.UNSPECIFIED.,.F.,.F.,(4,3,3,3,3,3,3,3,4),(-22.9415794419873,
-22.7303309946594,-21.742055734022,-20.7537804733847,-19.7655052127473,
-18.77722995211,-17.7889546914726,-16.8006794308352,-16.6583941348077),
 .UNSPECIFIED.);
#24407=B_SPLINE_CURVE_WITH_KNOTS('',3,(#104574,#104575,#104576,#104577,
#104578,#104579,#104580,#104581,#104582,#104583,#104584,#104585,#104586,
#104587,#104588,#104589,#104590,#104591,#104592,#104593,#104594,#104595,
#104596,#104597,#104598),.UNSPECIFIED.,.F.,.F.,(4,3,3,3,3,3,3,3,4),(13.6891124208201,
13.8358536489231,14.8241289095605,15.8124041701978,16.8006794308352,17.7889546914725,
18.7772299521099,19.7655052127473,19.9722977279997),.UNSPECIFIED.);
#24408=B_SPLINE_CURVE_WITH_KNOTS('',3,(#104603,#104604,#104605,#104606,
#104607,#104608,#104609,#104610,#104611,#104612,#104613,#104614,#104615,
#104616,#104617,#104618,#104619,#104620,#104621,#104622,#104623,#104624),
 .UNSPECIFIED.,.F.,.F.,(4,3,3,3,3,3,3,4),(-29.2247647491669,-28.6599825584836,
-27.6717072978462,-26.6834320372089,-25.6951567765715,-24.7068815159341,
-23.7186062552968,-22.9415794419873),.UNSPECIFIED.);
#24409=B_SPLINE_CURVE_WITH_KNOTS('',3,(#104625,#104626,#104627,#104628,
#104629,#104630,#104631,#104632,#104633,#104634,#104635,#104636,#104637,
#104638,#104639,#104640,#104641,#104642,#104643,#104644,#104645,#104646),
 .UNSPECIFIED.,.F.,.F.,(4,3,3,3,3,3,3,4),(19.9722977279997,20.7537804733846,
21.742055734022,22.7303309946594,23.7186062552967,24.7068815159341,25.6951567765715,
26.2554830351793),.UNSPECIFIED.);
#24410=B_SPLINE_CURVE_WITH_KNOTS('',3,(#104652,#104653,#104654,#104655,
#104656,#104657,#104658,#104659,#104660),.UNSPECIFIED.,.F.,.F.,(4,1,1,1,
1,1,4),(34.5575191894877,35.3345460027972,36.3228212634346,37.311096524072,
38.2993717847093,39.2876470453467,40.1793001539391),.UNSPECIFIED.);
#24411=B_SPLINE_CURVE_WITH_KNOTS('',3,(#104663,#104664,#104665,#104666,
#104667,#104668,#104669,#104670),.UNSPECIFIED.,.F.,.F.,(4,1,1,1,1,4),(34.5575191894877,
34.9854681915173,35.9737434521546,36.962018712792,37.9502939734294,38.9385692340667),
 .UNSPECIFIED.);
#24412=B_SPLINE_CURVE_WITH_KNOTS('',3,(#104675,#104676,#104677,#104678,
#104679,#104680,#104681,#104682,#104683,#104684,#104685),.UNSPECIFIED.,
 .F.,.F.,(4,1,1,1,1,1,1,1,4),(28.2743338823081,28.4166191783357,29.404894438973,
30.3931696996104,31.3814449602478,32.3697202208851,33.3579954815225,34.3462707421599,
34.5575191894877),.UNSPECIFIED.);
#24413=B_SPLINE_CURVE_WITH_KNOTS('',3,(#104686,#104687,#104688,#104689,
#104690,#104691,#104692,#104693,#104694,#104695),.UNSPECIFIED.,.F.,.F.,
(4,1,1,1,1,1,1,4),(28.2743338823081,29.0558166276931,30.0440918883304,31.0323671489678,
32.0206424096052,33.0089176702425,33.9971929308799,34.5575191894877),
 .UNSPECIFIED.);
#24414=B_SPLINE_CURVE_WITH_KNOTS('',3,(#104700,#104701,#104702,#104703,
#104704,#104705,#104706,#104707,#104708,#104709),.UNSPECIFIED.,.F.,.F.,
(4,1,1,1,1,1,1,4),(21.9911485751285,22.4869676145115,23.4752428751488,24.4635181357862,
25.4517933964236,26.4400686570609,27.4283439176983,28.2743338823081),
 .UNSPECIFIED.);
#24415=B_SPLINE_CURVE_WITH_KNOTS('',3,(#104710,#104711,#104712,#104713,
#104714,#104715,#104716,#104717,#104718,#104719,#104720),.UNSPECIFIED.,
 .F.,.F.,(4,1,1,1,1,1,1,1,4),(21.9911485751285,22.1378898032315,23.1261650638689,
24.1144403245063,25.1027155851436,26.090990845781,27.0792661064184,28.0675413670557,
28.2743338823081),.UNSPECIFIED.);
#24416=B_SPLINE_CURVE_WITH_KNOTS('',3,(#104725,#104726,#104727,#104728,
#104729,#104730,#104731,#104732,#104733,#104734),.UNSPECIFIED.,.F.,.F.,
(4,1,1,1,1,1,1,4),(15.707963267949,16.5573160506873,17.5455913113246,18.533866571962,
19.5221418325994,20.5104170932367,21.4986923538741,21.9911485751285),
 .UNSPECIFIED.);
#24417=B_SPLINE_CURVE_WITH_KNOTS('',3,(#104735,#104736,#104737,#104738,
#104739,#104740,#104741,#104742,#104743,#104744),.UNSPECIFIED.,.F.,.F.,
(4,1,1,1,1,1,1,4),(15.707963267949,16.2082382394074,17.1965135000447,18.1847887606821,
19.1730640213194,20.1613392819568,21.1496145425942,21.9911485751285),
 .UNSPECIFIED.);
#24418=B_SPLINE_CURVE_WITH_KNOTS('',3,(#104747,#104748,#104749,#104750,
#104751,#104752,#104753,#104754,#104755,#104756,#104757,#104758,#104759,
#104760,#104761,#104762,#104763,#104764,#104765,#104766,#104767,#104768,
#104769,#104770,#104771,#104772,#104773,#104774,#104775,#104776,#104777,
#104778,#104779,#104780,#104781,#104782,#104783,#104784,#104785,#104786,
#104787,#104788,#104789,#104790,#104791,#104792,#104793,#104794,#104795,
#104796,#104797,#104798,#104799,#104800,#104801,#104802,#104803,#104804,
#104805,#104806,#104807,#104808,#104809,#104810,#104811,#104812,#104813,
#104814,#104815,#104816,#104817,#104818,#104819,#104820,#104821,#104822,
#104823,#104824,#104825,#104826,#104827,#104828,#104829,#104830,#104831),
 .UNSPECIFIED.,.F.,.F.,(4,3,3,3,3,3,3,3,3,3,3,3,3,3,3,3,3,3,3,3,3,3,3,3,
3,3,3,3,4),(-0.276631791712739,-0.2650508057708,-0.250374720050919,-0.244981738899123,
-0.241597861612783,-0.226325618458574,-0.215430745967583,-0.211433653093672,
-0.208367227284489,-0.192603496037899,-0.17655849488178,-0.167210530793996,
-0.162395519488002,-0.159507286270078,-0.142982525939046,-0.139166638530642,
-0.123190507759063,-0.115491101024122,-0.110579056300749,-0.107660356137215,
-0.0911092121152923,-0.0741979921205997,-0.0647231249881659,-0.0582712594123912,
-0.0537680561212596,-0.0363099737577034,-0.0181549868788517,-0.00111529705586954,
0.),.UNSPECIFIED.);
#24419=B_SPLINE_CURVE_WITH_KNOTS('',3,(#104836,#104837,#104838,#104839,
#104840,#104841,#104842,#104843,#104844,#104845,#104846,#104847,#104848,
#104849,#104850,#104851,#104852,#104853,#104854,#104855,#104856,#104857,
#104858,#104859,#104860,#104861,#104862,#104863,#104864,#104865,#104866,
#104867,#104868,#104869,#104870,#104871,#104872,#104873,#104874,#104875,
#104876,#104877,#104878,#104879,#104880,#104881,#104882,#104883,#104884,
#104885,#104886,#104887,#104888,#104889,#104890,#104891,#104892,#104893,
#104894,#104895,#104896,#104897,#104898,#104899,#104900,#104901,#104902,
#104903,#104904,#104905,#104906,#104907,#104908,#104909,#104910,#104911,
#104912,#104913,#104914,#104915,#104916,#104917),.UNSPECIFIED.,.F.,.F.,
(4,3,3,3,3,3,3,3,3,3,3,3,3,3,3,3,3,3,3,3,3,3,3,3,3,3,3,4),(-0.275362278356874,
-0.261262622338533,-0.2441203930908,-0.237319173909909,-0.233882184799267,
-0.216686330248896,-0.205116137512367,-0.199379448294571,-0.195960066979035,
-0.179209945634759,-0.162881771419966,-0.153192525654141,-0.147976391807739,
-0.144164595227973,-0.128304665621163,-0.124124788356664,-0.108305429308661,
-0.100913932577369,-0.0956636604654543,-0.0926065387289381,-0.07684180355915,
-0.0611561838178058,-0.0532978747976696,-0.0475122493766209,-0.0447132850322838,
-0.0296095890058339,-0.014804794502917,0.),.UNSPECIFIED.);
#24420=B_SPLINE_CURVE_WITH_KNOTS('',3,(#105054,#105055,#105056,#105057,
#105058,#105059,#105060,#105061,#105062,#105063),.UNSPECIFIED.,.F.,.F.,
(4,3,3,4),(26.2554830351793,26.6834320372088,27.6717072978462,28.5633604064386),
 .UNSPECIFIED.);
#24421=B_SPLINE_CURVE_WITH_KNOTS('',3,(#105065,#105066,#105067,#105068,
#105069,#105070,#105071,#105072,#105073,#105074,#105075,#105076,#105077,
#105078,#105079,#105080,#105081,#105082,#105083,#105084,#105085,#105086,
#105087,#105088,#105089,#105090,#105091,#105092,#105093,#105094,#105095,
#105096,#105097,#105098,#105099,#105100,#105101,#105102,#105103,#105104,
#105105,#105106,#105107,#105108,#105109,#105110,#105111,#105112,#105113,
#105114,#105115,#105116,#105117,#105118,#105119,#105120,#105121,#105122,
#105123,#105124,#105125,#105126,#105127,#105128,#105129,#105130,#105131,
#105132,#105133,#105134,#105135,#105136,#105137,#105138,#105139,#105140,
#105141,#105142,#105143,#105144,#105145,#105146,#105147,#105148,#105149),
 .UNSPECIFIED.,.F.,.F.,(4,3,3,3,3,3,3,3,3,3,3,3,3,3,3,3,3,3,3,3,3,3,3,3,
3,3,3,3,4),(-0.276631791712748,-0.265050805770798,-0.250374723435734,-0.244981746785586,
-0.241597874545741,-0.226325633648081,-0.215430759258399,-0.211433696526451,
-0.208367237866174,-0.19260350809475,-0.176558506096897,-0.16721053920533,
-0.162395532418839,-0.159507299794083,-0.142982538633566,-0.139166638530629,
-0.12319050981671,-0.115491102953166,-0.110579056502434,-0.107660355608141,
-0.0911092140004719,-0.0741979961655583,-0.0647231241069456,-0.0582712562698588,
-0.0537680567287938,-0.0363099755898647,-0.0181549877949324,-0.00111528832129344,
0.),.UNSPECIFIED.);
#24422=B_SPLINE_CURVE_WITH_KNOTS('',3,(#105150,#105151,#105152,#105153,
#105154,#105155,#105156,#105157,#105158),.UNSPECIFIED.,.F.,.F.,(4,1,1,1,
1,1,4),(10.3752088276281,11.2668619362205,12.2551371968579,13.2434124574953,
14.2316877181326,15.21996297877,15.707963267949),.UNSPECIFIED.);
#24423=B_SPLINE_CURVE_WITH_KNOTS('',3,(#105164,#105165,#105166,#105167,
#105168,#105169,#105170,#105171,#105172,#105173,#105174,#105175,#105176,
#105177,#105178,#105179,#105180,#105181,#105182,#105183,#105184,#105185,
#105186,#105187,#105188,#105189,#105190,#105191,#105192,#105193,#105194,
#105195,#105196,#105197,#105198,#105199,#105200,#105201,#105202,#105203,
#105204,#105205,#105206,#105207,#105208,#105209,#105210,#105211,#105212,
#105213,#105214,#105215,#105216,#105217,#105218,#105219,#105220,#105221,
#105222,#105223,#105224,#105225,#105226,#105227,#105228,#105229,#105230,
#105231,#105232,#105233,#105234,#105235,#105236,#105237,#105238,#105239,
#105240,#105241,#105242,#105243,#105244,#105245),.UNSPECIFIED.,.F.,.F.,
(4,3,3,3,3,3,3,3,3,3,3,3,3,3,3,3,3,3,3,3,3,3,3,3,3,3,3,4),(-0.275362278356834,
-0.26126262233849,-0.244120393090759,-0.237319172495777,-0.233882181431016,
-0.216686326788785,-0.205116134484767,-0.199379437148685,-0.195960065205097,
-0.179209943129133,-0.162881764024476,-0.153192520107518,-0.147976388388869,
-0.144164594732856,-0.128304660393989,-0.124124788356646,-0.108305426694355,
-0.10091392976967,-0.0956636612369917,-0.0926065395413023,-0.0768418040865203,
-0.0611561896722693,-0.0532978771833044,-0.0475122544869175,-0.0447132896032582,
-0.0296096002398782,-0.0148048001199391,0.),.UNSPECIFIED.);
#24424=B_SPLINE_CURVE_WITH_KNOTS('',3,(#105248,#105249,#105250,#105251,
#105252,#105253,#105254,#105255),.UNSPECIFIED.,.F.,.F.,(4,1,1,1,1,4),(11.6159397475005,
12.6042150081378,13.5924902687752,14.5807655294126,15.5690407900499,15.707963267949),
 .UNSPECIFIED.);
#24425=B_SPLINE_CURVE_WITH_KNOTS('',3,(#105392,#105393,#105394,#105395,
#105396,#105397,#105398),.UNSPECIFIED.,.F.,.F.,(4,3,4),(-30.6365330797583,
-29.648257819121,-29.2247647491669),.UNSPECIFIED.);
#29677=VERTEX_POINT('',#104426);
#29678=VERTEX_POINT('',#104427);
#29679=VERTEX_POINT('',#104429);
#29680=VERTEX_POINT('',#104440);
#29681=VERTEX_POINT('',#104450);
#29682=VERTEX_POINT('',#104451);
#29683=VERTEX_POINT('',#104498);
#29684=VERTEX_POINT('',#104499);
#29685=VERTEX_POINT('',#104546);
#29686=VERTEX_POINT('',#104547);
#29687=VERTEX_POINT('',#104600);
#29688=VERTEX_POINT('',#104601);
#29689=VERTEX_POINT('',#104648);
#29690=VERTEX_POINT('',#104649);
#29691=VERTEX_POINT('',#104651);
#29692=VERTEX_POINT('',#104661);
#29693=VERTEX_POINT('',#104672);
#29694=VERTEX_POINT('',#104673);
#29695=VERTEX_POINT('',#104697);
#29696=VERTEX_POINT('',#104698);
#29697=VERTEX_POINT('',#104722);
#29698=VERTEX_POINT('',#104723);
#29699=VERTEX_POINT('',#104746);
#29700=VERTEX_POINT('',#104832);
#29701=VERTEX_POINT('',#104834);
#29702=VERTEX_POINT('',#105064);
#29703=VERTEX_POINT('',#105160);
#29704=VERTEX_POINT('',#105163);
#29705=VERTEX_POINT('',#105400);
#29706=VERTEX_POINT('',#105402);
#29707=VERTEX_POINT('',#105404);
#29708=VERTEX_POINT('',#105408);
#29709=VERTEX_POINT('',#105410);
#29710=VERTEX_POINT('',#105414);
#29711=VERTEX_POINT('',#105418);
#29712=VERTEX_POINT('',#105420);
#29713=VERTEX_POINT('',#105424);
#29714=VERTEX_POINT('',#105428);
#29715=VERTEX_POINT('',#105430);
#29716=VERTEX_POINT('',#105434);
#29717=VERTEX_POINT('',#105438);
#29718=VERTEX_POINT('',#105440);
#29719=VERTEX_POINT('',#105444);
#29720=VERTEX_POINT('',#105448);
#29721=VERTEX_POINT('',#105450);
#29722=VERTEX_POINT('',#105454);
#29723=VERTEX_POINT('',#105458);
#29724=VERTEX_POINT('',#105464);
#29725=VERTEX_POINT('',#105466);
#29726=VERTEX_POINT('',#105470);
#29727=VERTEX_POINT('',#105472);
#29728=VERTEX_POINT('',#105476);
#29729=VERTEX_POINT('',#105478);
#29730=VERTEX_POINT('',#105482);
#29731=VERTEX_POINT('',#105484);
#29732=VERTEX_POINT('',#105488);
#29733=VERTEX_POINT('',#105490);
#29734=VERTEX_POINT('',#105494);
#29735=VERTEX_POINT('',#105496);
#29736=VERTEX_POINT('',#105501);
#29737=VERTEX_POINT('',#105503);
#29738=VERTEX_POINT('',#105508);
#29739=VERTEX_POINT('',#105513);
#29740=VERTEX_POINT('',#105526);
#29741=VERTEX_POINT('',#105536);
#29742=VERTEX_POINT('',#105543);
#29743=VERTEX_POINT('',#105551);
#29744=VERTEX_POINT('',#105558);
#37982=EDGE_CURVE('',#29677,#29678,#16447,.T.);
#37983=EDGE_CURVE('',#29677,#29679,#24400,.T.);
#37984=EDGE_CURVE('',#29679,#29680,#1303,.T.);
#37985=EDGE_CURVE('',#29680,#29678,#24401,.T.);
#37986=EDGE_CURVE('',#29681,#29682,#16448,.T.);
#37987=EDGE_CURVE('',#29681,#29677,#24402,.T.);
#37988=EDGE_CURVE('',#29678,#29682,#24403,.T.);
#37989=EDGE_CURVE('',#29683,#29684,#16449,.T.);
#37990=EDGE_CURVE('',#29683,#29681,#24404,.T.);
#37991=EDGE_CURVE('',#29682,#29684,#24405,.T.);
#37992=EDGE_CURVE('',#29685,#29686,#16450,.T.);
#37993=EDGE_CURVE('',#29685,#29683,#24406,.T.);
#37994=EDGE_CURVE('',#29684,#29686,#24407,.T.);
#37995=EDGE_CURVE('',#29687,#29688,#16451,.T.);
#37996=EDGE_CURVE('',#29687,#29685,#24408,.T.);
#37997=EDGE_CURVE('',#29686,#29688,#24409,.T.);
#37998=EDGE_CURVE('',#29689,#29690,#16452,.T.);
#37999=EDGE_CURVE('',#29689,#29691,#24410,.T.);
#38000=EDGE_CURVE('',#29692,#29691,#1304,.T.);
#38001=EDGE_CURVE('',#29690,#29692,#24411,.T.);
#38002=EDGE_CURVE('',#29693,#29694,#16453,.T.);
#38003=EDGE_CURVE('',#29693,#29689,#24412,.T.);
#38004=EDGE_CURVE('',#29694,#29690,#24413,.T.);
#38005=EDGE_CURVE('',#29695,#29696,#16454,.T.);
#38006=EDGE_CURVE('',#29695,#29693,#24414,.T.);
#38007=EDGE_CURVE('',#29696,#29694,#24415,.T.);
#38008=EDGE_CURVE('',#29697,#29698,#16455,.T.);
#38009=EDGE_CURVE('',#29697,#29695,#24416,.T.);
#38010=EDGE_CURVE('',#29698,#29696,#24417,.T.);
#38011=EDGE_CURVE('',#29691,#29699,#24418,.T.);
#38012=EDGE_CURVE('',#29700,#29699,#1305,.F.);
#38013=EDGE_CURVE('',#29701,#29700,#1306,.F.);
#38014=EDGE_CURVE('',#29701,#29692,#24419,.T.);
#38015=EDGE_CURVE('',#29688,#29701,#24420,.T.);
#38016=EDGE_CURVE('',#29702,#29680,#24421,.T.);
#38017=EDGE_CURVE('',#29702,#29698,#24422,.T.);
#38018=EDGE_CURVE('',#29680,#29703,#1307,.T.);
#38019=EDGE_CURVE('',#29703,#29679,#1308,.T.);
#38020=EDGE_CURVE('',#29679,#29704,#24423,.T.);
#38021=EDGE_CURVE('',#29704,#29702,#1309,.T.);
#38022=EDGE_CURVE('',#29704,#29697,#24424,.T.);
#38023=EDGE_CURVE('',#29699,#29687,#24425,.T.);
#38024=EDGE_CURVE('',#29705,#29705,#1310,.T.);
#38025=EDGE_CURVE('',#29705,#29706,#16456,.T.);
#38026=EDGE_CURVE('',#29707,#29706,#383,.T.);
#38027=EDGE_CURVE('',#29707,#29708,#1311,.T.);
#38028=EDGE_CURVE('',#29709,#29708,#384,.T.);
#38029=EDGE_CURVE('',#29710,#29709,#385,.T.);
#38030=EDGE_CURVE('',#29710,#29711,#1312,.T.);
#38031=EDGE_CURVE('',#29712,#29711,#386,.T.);
#38032=EDGE_CURVE('',#29713,#29712,#387,.T.);
#38033=EDGE_CURVE('',#29713,#29714,#1313,.T.);
#38034=EDGE_CURVE('',#29715,#29714,#388,.T.);
#38035=EDGE_CURVE('',#29716,#29715,#389,.T.);
#38036=EDGE_CURVE('',#29716,#29717,#1314,.T.);
#38037=EDGE_CURVE('',#29718,#29717,#390,.T.);
#38038=EDGE_CURVE('',#29719,#29718,#391,.T.);
#38039=EDGE_CURVE('',#29719,#29720,#1315,.T.);
#38040=EDGE_CURVE('',#29721,#29720,#392,.T.);
#38041=EDGE_CURVE('',#29722,#29721,#393,.T.);
#38042=EDGE_CURVE('',#29722,#29723,#1316,.T.);
#38043=EDGE_CURVE('',#29706,#29723,#394,.T.);
#38044=EDGE_CURVE('',#29711,#29724,#16457,.T.);
#38045=EDGE_CURVE('',#29725,#29710,#16458,.T.);
#38046=EDGE_CURVE('',#29724,#29725,#1317,.T.);
#38047=EDGE_CURVE('',#29714,#29726,#16459,.T.);
#38048=EDGE_CURVE('',#29727,#29713,#16460,.T.);
#38049=EDGE_CURVE('',#29726,#29727,#1318,.T.);
#38050=EDGE_CURVE('',#29728,#29707,#16461,.T.);
#38051=EDGE_CURVE('',#29729,#29728,#1319,.T.);
#38052=EDGE_CURVE('',#29708,#29729,#16462,.T.);
#38053=EDGE_CURVE('',#29717,#29730,#16463,.T.);
#38054=EDGE_CURVE('',#29731,#29716,#16464,.T.);
#38055=EDGE_CURVE('',#29730,#29731,#1320,.T.);
#38056=EDGE_CURVE('',#29732,#29722,#16465,.T.);
#38057=EDGE_CURVE('',#29733,#29732,#1321,.T.);
#38058=EDGE_CURVE('',#29723,#29733,#16466,.T.);
#38059=EDGE_CURVE('',#29734,#29719,#16467,.T.);
#38060=EDGE_CURVE('',#29735,#29734,#1322,.T.);
#38061=EDGE_CURVE('',#29720,#29735,#16468,.T.);
#38062=EDGE_CURVE('',#29731,#29730,#16469,.T.);
#38063=EDGE_CURVE('',#29715,#29736,#16470,.T.);
#38064=EDGE_CURVE('',#29736,#29737,#16471,.T.);
#38065=EDGE_CURVE('',#29718,#29737,#16472,.T.);
#38066=EDGE_CURVE('',#29727,#29726,#16473,.T.);
#38067=EDGE_CURVE('',#29712,#29738,#16474,.T.);
#38068=EDGE_CURVE('',#29738,#29736,#16475,.T.);
#38069=EDGE_CURVE('',#29725,#29724,#16476,.T.);
#38070=EDGE_CURVE('',#29709,#29739,#16477,.T.);
#38071=EDGE_CURVE('',#29739,#29738,#16478,.T.);
#38072=EDGE_CURVE('',#29728,#29729,#16479,.T.);
#38073=EDGE_CURVE('',#29732,#29733,#16480,.T.);
#38074=EDGE_CURVE('',#29734,#29735,#16481,.T.);
#38075=EDGE_CURVE('',#29740,#29739,#16482,.T.);
#38076=EDGE_CURVE('',#29740,#29739,#1323,.T.);
#38077=EDGE_CURVE('',#29739,#29738,#1324,.T.);
#38078=EDGE_CURVE('',#29738,#29736,#1325,.T.);
#38079=EDGE_CURVE('',#29736,#29737,#1326,.T.);
#38080=EDGE_CURVE('',#29737,#29741,#16483,.T.);
#38081=EDGE_CURVE('',#29737,#29741,#1327,.T.);
#38082=EDGE_CURVE('',#29741,#29740,#16484,.T.);
#38083=EDGE_CURVE('',#29741,#29740,#1328,.T.);
#38084=EDGE_CURVE('',#29740,#29742,#16485,.T.);
#38085=EDGE_CURVE('',#29706,#29740,#16486,.T.);
#38086=EDGE_CURVE('',#29721,#29741,#16487,.T.);
#38087=EDGE_CURVE('',#29743,#29743,#1329,.T.);
#38088=EDGE_CURVE('',#29703,#29743,#16488,.T.);
#38089=EDGE_CURVE('',#29699,#29701,#1330,.F.);
#38090=EDGE_CURVE('',#29744,#29744,#1331,.T.);
#38091=EDGE_CURVE('',#29744,#29700,#16489,.T.);
#54299=ORIENTED_EDGE('',*,*,#37982,.F.);
#54300=ORIENTED_EDGE('',*,*,#37983,.T.);
#54301=ORIENTED_EDGE('',*,*,#37984,.T.);
#54302=ORIENTED_EDGE('',*,*,#37985,.T.);
#54303=ORIENTED_EDGE('',*,*,#37986,.F.);
#54304=ORIENTED_EDGE('',*,*,#37987,.T.);
#54305=ORIENTED_EDGE('',*,*,#37982,.T.);
#54306=ORIENTED_EDGE('',*,*,#37988,.T.);
#54307=ORIENTED_EDGE('',*,*,#37989,.F.);
#54308=ORIENTED_EDGE('',*,*,#37990,.T.);
#54309=ORIENTED_EDGE('',*,*,#37986,.T.);
#54310=ORIENTED_EDGE('',*,*,#37991,.T.);
#54311=ORIENTED_EDGE('',*,*,#37992,.F.);
#54312=ORIENTED_EDGE('',*,*,#37993,.T.);
#54313=ORIENTED_EDGE('',*,*,#37989,.T.);
#54314=ORIENTED_EDGE('',*,*,#37994,.T.);
#54315=ORIENTED_EDGE('',*,*,#37995,.F.);
#54316=ORIENTED_EDGE('',*,*,#37996,.T.);
#54317=ORIENTED_EDGE('',*,*,#37992,.T.);
#54318=ORIENTED_EDGE('',*,*,#37997,.T.);
#54319=ORIENTED_EDGE('',*,*,#37998,.F.);
#54320=ORIENTED_EDGE('',*,*,#37999,.T.);
#54321=ORIENTED_EDGE('',*,*,#38000,.F.);
#54322=ORIENTED_EDGE('',*,*,#38001,.F.);
#54323=ORIENTED_EDGE('',*,*,#38002,.F.);
#54324=ORIENTED_EDGE('',*,*,#38003,.T.);
#54325=ORIENTED_EDGE('',*,*,#37998,.T.);
#54326=ORIENTED_EDGE('',*,*,#38004,.F.);
#54327=ORIENTED_EDGE('',*,*,#38005,.F.);
#54328=ORIENTED_EDGE('',*,*,#38006,.T.);
#54329=ORIENTED_EDGE('',*,*,#38002,.T.);
#54330=ORIENTED_EDGE('',*,*,#38007,.F.);
#54331=ORIENTED_EDGE('',*,*,#38008,.F.);
#54332=ORIENTED_EDGE('',*,*,#38009,.T.);
#54333=ORIENTED_EDGE('',*,*,#38005,.T.);
#54334=ORIENTED_EDGE('',*,*,#38010,.F.);
#54335=ORIENTED_EDGE('',*,*,#38000,.T.);
#54336=ORIENTED_EDGE('',*,*,#38011,.T.);
#54337=ORIENTED_EDGE('',*,*,#38012,.F.);
#54338=ORIENTED_EDGE('',*,*,#38013,.F.);
#54339=ORIENTED_EDGE('',*,*,#38014,.T.);
#54340=ORIENTED_EDGE('',*,*,#38014,.F.);
#54341=ORIENTED_EDGE('',*,*,#38015,.F.);
#54342=ORIENTED_EDGE('',*,*,#37997,.F.);
#54343=ORIENTED_EDGE('',*,*,#37994,.F.);
#54344=ORIENTED_EDGE('',*,*,#37991,.F.);
#54345=ORIENTED_EDGE('',*,*,#37988,.F.);
#54346=ORIENTED_EDGE('',*,*,#37985,.F.);
#54347=ORIENTED_EDGE('',*,*,#38016,.F.);
#54348=ORIENTED_EDGE('',*,*,#38017,.T.);
#54349=ORIENTED_EDGE('',*,*,#38010,.T.);
#54350=ORIENTED_EDGE('',*,*,#38007,.T.);
#54351=ORIENTED_EDGE('',*,*,#38004,.T.);
#54352=ORIENTED_EDGE('',*,*,#38001,.T.);
#54353=ORIENTED_EDGE('',*,*,#38018,.T.);
#54354=ORIENTED_EDGE('',*,*,#38019,.T.);
#54355=ORIENTED_EDGE('',*,*,#38020,.T.);
#54356=ORIENTED_EDGE('',*,*,#38021,.T.);
#54357=ORIENTED_EDGE('',*,*,#38016,.T.);
#54358=ORIENTED_EDGE('',*,*,#38008,.T.);
#54359=ORIENTED_EDGE('',*,*,#38017,.F.);
#54360=ORIENTED_EDGE('',*,*,#38021,.F.);
#54361=ORIENTED_EDGE('',*,*,#38022,.T.);
#54362=ORIENTED_EDGE('',*,*,#38011,.F.);
#54363=ORIENTED_EDGE('',*,*,#37999,.F.);
#54364=ORIENTED_EDGE('',*,*,#38003,.F.);
#54365=ORIENTED_EDGE('',*,*,#38006,.F.);
#54366=ORIENTED_EDGE('',*,*,#38009,.F.);
#54367=ORIENTED_EDGE('',*,*,#38022,.F.);
#54368=ORIENTED_EDGE('',*,*,#38020,.F.);
#54369=ORIENTED_EDGE('',*,*,#37983,.F.);
#54370=ORIENTED_EDGE('',*,*,#37987,.F.);
#54371=ORIENTED_EDGE('',*,*,#37990,.F.);
#54372=ORIENTED_EDGE('',*,*,#37993,.F.);
#54373=ORIENTED_EDGE('',*,*,#37996,.F.);
#54374=ORIENTED_EDGE('',*,*,#38023,.F.);
#54375=ORIENTED_EDGE('',*,*,#38024,.F.);
#54376=ORIENTED_EDGE('',*,*,#38025,.T.);
#54377=ORIENTED_EDGE('',*,*,#38026,.F.);
#54378=ORIENTED_EDGE('',*,*,#38027,.T.);
#54379=ORIENTED_EDGE('',*,*,#38028,.F.);
#54380=ORIENTED_EDGE('',*,*,#38029,.F.);
#54381=ORIENTED_EDGE('',*,*,#38030,.T.);
#54382=ORIENTED_EDGE('',*,*,#38031,.F.);
#54383=ORIENTED_EDGE('',*,*,#38032,.F.);
#54384=ORIENTED_EDGE('',*,*,#38033,.T.);
#54385=ORIENTED_EDGE('',*,*,#38034,.F.);
#54386=ORIENTED_EDGE('',*,*,#38035,.F.);
#54387=ORIENTED_EDGE('',*,*,#38036,.T.);
#54388=ORIENTED_EDGE('',*,*,#38037,.F.);
#54389=ORIENTED_EDGE('',*,*,#38038,.F.);
#54390=ORIENTED_EDGE('',*,*,#38039,.T.);
#54391=ORIENTED_EDGE('',*,*,#38040,.F.);
#54392=ORIENTED_EDGE('',*,*,#38041,.F.);
#54393=ORIENTED_EDGE('',*,*,#38042,.T.);
#54394=ORIENTED_EDGE('',*,*,#38043,.F.);
#54395=ORIENTED_EDGE('',*,*,#38025,.F.);
#54396=ORIENTED_EDGE('',*,*,#38044,.F.);
#54397=ORIENTED_EDGE('',*,*,#38030,.F.);
#54398=ORIENTED_EDGE('',*,*,#38045,.F.);
#54399=ORIENTED_EDGE('',*,*,#38046,.F.);
#54400=ORIENTED_EDGE('',*,*,#38047,.F.);
#54401=ORIENTED_EDGE('',*,*,#38033,.F.);
#54402=ORIENTED_EDGE('',*,*,#38048,.F.);
#54403=ORIENTED_EDGE('',*,*,#38049,.F.);
#54404=ORIENTED_EDGE('',*,*,#38050,.F.);
#54405=ORIENTED_EDGE('',*,*,#38051,.F.);
#54406=ORIENTED_EDGE('',*,*,#38052,.F.);
#54407=ORIENTED_EDGE('',*,*,#38027,.F.);
#54408=ORIENTED_EDGE('',*,*,#38053,.F.);
#54409=ORIENTED_EDGE('',*,*,#38036,.F.);
#54410=ORIENTED_EDGE('',*,*,#38054,.F.);
#54411=ORIENTED_EDGE('',*,*,#38055,.F.);
#54412=ORIENTED_EDGE('',*,*,#38056,.F.);
#54413=ORIENTED_EDGE('',*,*,#38057,.F.);
#54414=ORIENTED_EDGE('',*,*,#38058,.F.);
#54415=ORIENTED_EDGE('',*,*,#38042,.F.);
#54416=ORIENTED_EDGE('',*,*,#38059,.F.);
#54417=ORIENTED_EDGE('',*,*,#38060,.F.);
#54418=ORIENTED_EDGE('',*,*,#38061,.F.);
#54419=ORIENTED_EDGE('',*,*,#38039,.F.);
#54420=ORIENTED_EDGE('',*,*,#38037,.T.);
#54421=ORIENTED_EDGE('',*,*,#38053,.T.);
#54422=ORIENTED_EDGE('',*,*,#38062,.F.);
#54423=ORIENTED_EDGE('',*,*,#38054,.T.);
#54424=ORIENTED_EDGE('',*,*,#38035,.T.);
#54425=ORIENTED_EDGE('',*,*,#38063,.T.);
#54426=ORIENTED_EDGE('',*,*,#38064,.T.);
#54427=ORIENTED_EDGE('',*,*,#38065,.F.);
#54428=ORIENTED_EDGE('',*,*,#38034,.T.);
#54429=ORIENTED_EDGE('',*,*,#38047,.T.);
#54430=ORIENTED_EDGE('',*,*,#38066,.F.);
#54431=ORIENTED_EDGE('',*,*,#38048,.T.);
#54432=ORIENTED_EDGE('',*,*,#38032,.T.);
#54433=ORIENTED_EDGE('',*,*,#38067,.T.);
#54434=ORIENTED_EDGE('',*,*,#38068,.T.);
#54435=ORIENTED_EDGE('',*,*,#38063,.F.);
#54436=ORIENTED_EDGE('',*,*,#38031,.T.);
#54437=ORIENTED_EDGE('',*,*,#38044,.T.);
#54438=ORIENTED_EDGE('',*,*,#38069,.F.);
#54439=ORIENTED_EDGE('',*,*,#38045,.T.);
#54440=ORIENTED_EDGE('',*,*,#38029,.T.);
#54441=ORIENTED_EDGE('',*,*,#38070,.T.);
#54442=ORIENTED_EDGE('',*,*,#38071,.T.);
#54443=ORIENTED_EDGE('',*,*,#38067,.F.);
#54444=ORIENTED_EDGE('',*,*,#38046,.T.);
#54445=ORIENTED_EDGE('',*,*,#38069,.T.);
#54446=ORIENTED_EDGE('',*,*,#38049,.T.);
#54447=ORIENTED_EDGE('',*,*,#38066,.T.);
#54448=ORIENTED_EDGE('',*,*,#38051,.T.);
#54449=ORIENTED_EDGE('',*,*,#38072,.T.);
#54450=ORIENTED_EDGE('',*,*,#38055,.T.);
#54451=ORIENTED_EDGE('',*,*,#38062,.T.);
#54452=ORIENTED_EDGE('',*,*,#38057,.T.);
#54453=ORIENTED_EDGE('',*,*,#38073,.T.);
#54454=ORIENTED_EDGE('',*,*,#38060,.T.);
#54455=ORIENTED_EDGE('',*,*,#38074,.T.);
#54456=ORIENTED_EDGE('',*,*,#38075,.F.);
#54457=ORIENTED_EDGE('',*,*,#38076,.T.);
#54458=ORIENTED_EDGE('',*,*,#38071,.F.);
#54459=ORIENTED_EDGE('',*,*,#38077,.T.);
#54460=ORIENTED_EDGE('',*,*,#38068,.F.);
#54461=ORIENTED_EDGE('',*,*,#38078,.T.);
#54462=ORIENTED_EDGE('',*,*,#38064,.F.);
#54463=ORIENTED_EDGE('',*,*,#38079,.T.);
#54464=ORIENTED_EDGE('',*,*,#38080,.F.);
#54465=ORIENTED_EDGE('',*,*,#38081,.T.);
#54466=ORIENTED_EDGE('',*,*,#38082,.F.);
#54467=ORIENTED_EDGE('',*,*,#38083,.T.);
#54468=ORIENTED_EDGE('',*,*,#38079,.F.);
#54469=ORIENTED_EDGE('',*,*,#38078,.F.);
#54470=ORIENTED_EDGE('',*,*,#38077,.F.);
#54471=ORIENTED_EDGE('',*,*,#38076,.F.);
#54472=ORIENTED_EDGE('',*,*,#38084,.T.);
#54473=ORIENTED_EDGE('',*,*,#38084,.F.);
#54474=ORIENTED_EDGE('',*,*,#38083,.F.);
#54475=ORIENTED_EDGE('',*,*,#38081,.F.);
#54476=ORIENTED_EDGE('',*,*,#38026,.T.);
#54477=ORIENTED_EDGE('',*,*,#38085,.T.);
#54478=ORIENTED_EDGE('',*,*,#38075,.T.);
#54479=ORIENTED_EDGE('',*,*,#38070,.F.);
#54480=ORIENTED_EDGE('',*,*,#38028,.T.);
#54481=ORIENTED_EDGE('',*,*,#38052,.T.);
#54482=ORIENTED_EDGE('',*,*,#38072,.F.);
#54483=ORIENTED_EDGE('',*,*,#38050,.T.);
#54484=ORIENTED_EDGE('',*,*,#38041,.T.);
#54485=ORIENTED_EDGE('',*,*,#38086,.T.);
#54486=ORIENTED_EDGE('',*,*,#38082,.T.);
#54487=ORIENTED_EDGE('',*,*,#38085,.F.);
#54488=ORIENTED_EDGE('',*,*,#38043,.T.);
#54489=ORIENTED_EDGE('',*,*,#38058,.T.);
#54490=ORIENTED_EDGE('',*,*,#38073,.F.);
#54491=ORIENTED_EDGE('',*,*,#38056,.T.);
#54492=ORIENTED_EDGE('',*,*,#38038,.T.);
#54493=ORIENTED_EDGE('',*,*,#38065,.T.);
#54494=ORIENTED_EDGE('',*,*,#38080,.T.);
#54495=ORIENTED_EDGE('',*,*,#38086,.F.);
#54496=ORIENTED_EDGE('',*,*,#38040,.T.);
#54497=ORIENTED_EDGE('',*,*,#38061,.T.);
#54498=ORIENTED_EDGE('',*,*,#38074,.F.);
#54499=ORIENTED_EDGE('',*,*,#38059,.T.);
#54500=ORIENTED_EDGE('',*,*,#38087,.F.);
#54501=ORIENTED_EDGE('',*,*,#38024,.T.);
#54502=ORIENTED_EDGE('',*,*,#38018,.F.);
#54503=ORIENTED_EDGE('',*,*,#37984,.F.);
#54504=ORIENTED_EDGE('',*,*,#38019,.F.);
#54505=ORIENTED_EDGE('',*,*,#38088,.T.);
#54506=ORIENTED_EDGE('',*,*,#38087,.T.);
#54507=ORIENTED_EDGE('',*,*,#38088,.F.);
#54508=ORIENTED_EDGE('',*,*,#37995,.T.);
#54509=ORIENTED_EDGE('',*,*,#38015,.T.);
#54510=ORIENTED_EDGE('',*,*,#38089,.F.);
#54511=ORIENTED_EDGE('',*,*,#38023,.T.);
#54512=ORIENTED_EDGE('',*,*,#38090,.F.);
#54513=ORIENTED_EDGE('',*,*,#38091,.T.);
#54514=ORIENTED_EDGE('',*,*,#38012,.T.);
#54515=ORIENTED_EDGE('',*,*,#38089,.T.);
#54516=ORIENTED_EDGE('',*,*,#38013,.T.);
#54517=ORIENTED_EDGE('',*,*,#38091,.F.);
#54518=ORIENTED_EDGE('',*,*,#38090,.T.);
#57113=B_SPLINE_SURFACE_WITH_KNOTS('',3,3,((#104918,#104919,#104920,#104921,
#104922,#104923,#104924,#104925,#104926,#104927,#104928,#104929,#104930,
#104931,#104932,#104933,#104934,#104935,#104936,#104937,#104938,#104939,
#104940,#104941,#104942,#104943,#104944,#104945,#104946,#104947,#104948,
#104949,#104950,#104951),(#104952,#104953,#104954,#104955,#104956,#104957,
#104958,#104959,#104960,#104961,#104962,#104963,#104964,#104965,#104966,
#104967,#104968,#104969,#104970,#104971,#104972,#104973,#104974,#104975,
#104976,#104977,#104978,#104979,#104980,#104981,#104982,#104983,#104984,
#104985),(#104986,#104987,#104988,#104989,#104990,#104991,#104992,#104993,
#104994,#104995,#104996,#104997,#104998,#104999,#105000,#105001,#105002,
#105003,#105004,#105005,#105006,#105007,#105008,#105009,#105010,#105011,
#105012,#105013,#105014,#105015,#105016,#105017,#105018,#105019),(#105020,
#105021,#105022,#105023,#105024,#105025,#105026,#105027,#105028,#105029,
#105030,#105031,#105032,#105033,#105034,#105035,#105036,#105037,#105038,
#105039,#105040,#105041,#105042,#105043,#105044,#105045,#105046,#105047,
#105048,#105049,#105050,#105051,#105052,#105053)),.UNSPECIFIED.,.F.,.F.,
 .F.,(4,4),(4,1,1,1,1,1,1,1,1,1,1,1,1,1,1,1,1,1,1,1,1,1,1,1,1,1,1,1,1,1,
1,4),(0.,0.032995567884187),(8.30203615430844,9.2903114149458,10.2785866755832,
11.2668619362205,12.2551371968579,13.2434124574953,14.2316877181326,15.21996297877,
16.2082382394074,17.1965135000447,18.1847887606821,19.1730640213194,20.1613392819568,
21.1496145425942,22.1378898032315,23.1261650638689,24.1144403245063,25.1027155851436,
26.090990845781,27.0792661064184,28.0675413670557,29.0558166276931,30.0440918883304,
31.0323671489678,32.0206424096052,33.0089176702425,33.9971929308799,34.9854681915173,
35.9737434521546,36.962018712792,37.9502939734294,38.9385692340667),
 .UNSPECIFIED.);
#57114=B_SPLINE_SURFACE_WITH_KNOTS('',3,3,((#105256,#105257,#105258,#105259,
#105260,#105261,#105262,#105263,#105264,#105265,#105266,#105267,#105268,
#105269,#105270,#105271,#105272,#105273,#105274,#105275,#105276,#105277,
#105278,#105279,#105280,#105281,#105282,#105283,#105284,#105285,#105286,
#105287,#105288,#105289),(#105290,#105291,#105292,#105293,#105294,#105295,
#105296,#105297,#105298,#105299,#105300,#105301,#105302,#105303,#105304,
#105305,#105306,#105307,#105308,#105309,#105310,#105311,#105312,#105313,
#105314,#105315,#105316,#105317,#105318,#105319,#105320,#105321,#105322,
#105323),(#105324,#105325,#105326,#105327,#105328,#105329,#105330,#105331,
#105332,#105333,#105334,#105335,#105336,#105337,#105338,#105339,#105340,
#105341,#105342,#105343,#105344,#105345,#105346,#105347,#105348,#105349,
#105350,#105351,#105352,#105353,#105354,#105355,#105356,#105357),(#105358,
#105359,#105360,#105361,#105362,#105363,#105364,#105365,#105366,#105367,
#105368,#105369,#105370,#105371,#105372,#105373,#105374,#105375,#105376,
#105377,#105378,#105379,#105380,#105381,#105382,#105383,#105384,#105385,
#105386,#105387,#105388,#105389,#105390,#105391)),.UNSPECIFIED.,.F.,.F.,
 .F.,(4,4),(4,1,1,1,1,1,1,1,1,1,1,1,1,1,1,1,1,1,1,1,1,1,1,1,1,1,1,1,1,1,
1,4),(0.,0.032995567884187),(11.6159397475005,12.6042150081378,13.5924902687752,
14.5807655294126,15.5690407900499,16.5573160506873,17.5455913113246,18.533866571962,
19.5221418325994,20.5104170932367,21.4986923538741,22.4869676145115,23.4752428751488,
24.4635181357862,25.4517933964236,26.4400686570609,27.4283439176983,28.4166191783357,
29.404894438973,30.3931696996104,31.3814449602478,32.3697202208851,33.3579954815225,
34.3462707421599,35.3345460027972,36.3228212634346,37.311096524072,38.2993717847093,
39.2876470453467,40.2759223059841,41.2641975666214,42.2524728272588),
 .UNSPECIFIED.);
#59989=ADVANCED_FACE('',(#6889),#742,.T.);
#59990=ADVANCED_FACE('',(#6890),#743,.T.);
#59991=ADVANCED_FACE('',(#6891),#744,.T.);
#59992=ADVANCED_FACE('',(#6892),#745,.T.);
#59993=ADVANCED_FACE('',(#6893),#746,.T.);
#59994=ADVANCED_FACE('',(#6894),#747,.T.);
#59995=ADVANCED_FACE('',(#6895),#748,.T.);
#59996=ADVANCED_FACE('',(#6896),#749,.T.);
#59997=ADVANCED_FACE('',(#6897),#750,.T.);
#59998=ADVANCED_FACE('',(#6898),#3793,.T.);
#59999=ADVANCED_FACE('',(#6899),#57113,.F.);
#60000=ADVANCED_FACE('',(#6900),#3794,.F.);
#60001=ADVANCED_FACE('',(#6901),#751,.T.);
#60002=ADVANCED_FACE('',(#6902),#57114,.F.);
#60003=ADVANCED_FACE('',(#6903),#933,.F.);
#60004=ADVANCED_FACE('',(#6904),#752,.T.);
#60005=ADVANCED_FACE('',(#6905),#753,.T.);
#60006=ADVANCED_FACE('',(#6906),#754,.T.);
#60007=ADVANCED_FACE('',(#6907),#755,.T.);
#60008=ADVANCED_FACE('',(#6908),#756,.T.);
#60009=ADVANCED_FACE('',(#6909),#757,.T.);
#60010=ADVANCED_FACE('',(#6910),#3795,.F.);
#60011=ADVANCED_FACE('',(#6911),#3796,.F.);
#60012=ADVANCED_FACE('',(#6912),#3797,.F.);
#60013=ADVANCED_FACE('',(#6913),#3798,.T.);
#60014=ADVANCED_FACE('',(#6914),#3799,.T.);
#60015=ADVANCED_FACE('',(#6915),#3800,.T.);
#60016=ADVANCED_FACE('',(#6916),#3801,.T.);
#60017=ADVANCED_FACE('',(#6917),#3802,.T.);
#60018=ADVANCED_FACE('',(#6918),#3803,.T.);
#60019=ADVANCED_FACE('',(#6919),#3804,.F.);
#60020=ADVANCED_FACE('',(#6920),#3805,.F.);
#60021=ADVANCED_FACE('',(#6921),#3806,.F.);
#60022=ADVANCED_FACE('',(#6922),#3807,.F.);
#60023=ADVANCED_FACE('',(#6923),#3808,.F.);
#60024=ADVANCED_FACE('',(#6924),#3809,.F.);
#60025=ADVANCED_FACE('',(#6925),#934,.F.);
#60026=ADVANCED_FACE('',(#6926),#3810,.F.);
#60027=ADVANCED_FACE('',(#6927),#3811,.F.);
#60028=ADVANCED_FACE('',(#6928),#3812,.F.);
#60029=ADVANCED_FACE('',(#6929,#1852),#3813,.T.);
#60030=ADVANCED_FACE('',(#6930),#935,.T.);
#60031=ADVANCED_FACE('',(#6931),#758,.T.);
#60032=ADVANCED_FACE('',(#6932),#936,.T.);
#60033=ADVANCED_FACE('',(#6933),#3814,.T.);
#60403=CLOSED_SHELL('',(#59989,#59990,#59991,#59992,#59993,#59994,#59995,
#59996,#59997,#59998,#59999,#60000,#60001,#60002,#60003,#60004,#60005,#60006,
#60007,#60008,#60009,#60010,#60011,#60012,#60013,#60014,#60015,#60016,#60017,
#60018,#60019,#60020,#60021,#60022,#60023,#60024,#60025,#60026,#60027,#60028,
#60029,#60030,#60031,#60032,#60033));
#63115=AXIS2_PLACEMENT_3D('',#104424,#74359,#74360);
#63116=AXIS2_PLACEMENT_3D('',#104425,#74361,#74362);
#63117=AXIS2_PLACEMENT_3D('',#104441,#74364,#74365);
#63118=AXIS2_PLACEMENT_3D('',#104449,#74366,#74367);
#63119=AXIS2_PLACEMENT_3D('',#104497,#74369,#74370);
#63120=AXIS2_PLACEMENT_3D('',#104545,#74372,#74373);
#63121=AXIS2_PLACEMENT_3D('',#104599,#74375,#74376);
#63122=AXIS2_PLACEMENT_3D('',#104647,#74378,#74379);
#63123=AXIS2_PLACEMENT_3D('',#104662,#74381,#74382);
#63124=AXIS2_PLACEMENT_3D('',#104671,#74383,#74384);
#63125=AXIS2_PLACEMENT_3D('',#104696,#74386,#74387);
#63126=AXIS2_PLACEMENT_3D('',#104721,#74389,#74390);
#63127=AXIS2_PLACEMENT_3D('',#104745,#74392,#74393);
#63128=AXIS2_PLACEMENT_3D('',#104833,#74394,#74395);
#63129=AXIS2_PLACEMENT_3D('',#104835,#74396,#74397);
#63130=AXIS2_PLACEMENT_3D('',#105159,#74398,#74399);
#63131=AXIS2_PLACEMENT_3D('',#105161,#74400,#74401);
#63132=AXIS2_PLACEMENT_3D('',#105162,#74402,#74403);
#63133=AXIS2_PLACEMENT_3D('',#105246,#74404,#74405);
#63134=AXIS2_PLACEMENT_3D('',#105247,#74406,#74407);
#63135=AXIS2_PLACEMENT_3D('',#105399,#74408,#74409);
#63136=AXIS2_PLACEMENT_3D('',#105401,#74410,#74411);
#63137=AXIS2_PLACEMENT_3D('',#105409,#74413,#74414);
#63138=AXIS2_PLACEMENT_3D('',#105419,#74415,#74416);
#63139=AXIS2_PLACEMENT_3D('',#105429,#74417,#74418);
#63140=AXIS2_PLACEMENT_3D('',#105439,#74419,#74420);
#63141=AXIS2_PLACEMENT_3D('',#105449,#74421,#74422);
#63142=AXIS2_PLACEMENT_3D('',#105459,#74423,#74424);
#63143=AXIS2_PLACEMENT_3D('',#105463,#74425,#74426);
#63144=AXIS2_PLACEMENT_3D('',#105468,#74429,#74430);
#63145=AXIS2_PLACEMENT_3D('',#105469,#74431,#74432);
#63146=AXIS2_PLACEMENT_3D('',#105474,#74435,#74436);
#63147=AXIS2_PLACEMENT_3D('',#105475,#74437,#74438);
#63148=AXIS2_PLACEMENT_3D('',#105479,#74440,#74441);
#63149=AXIS2_PLACEMENT_3D('',#105481,#74443,#74444);
#63150=AXIS2_PLACEMENT_3D('',#105486,#74447,#74448);
#63151=AXIS2_PLACEMENT_3D('',#105487,#74449,#74450);
#63152=AXIS2_PLACEMENT_3D('',#105491,#74452,#74453);
#63153=AXIS2_PLACEMENT_3D('',#105493,#74455,#74456);
#63154=AXIS2_PLACEMENT_3D('',#105497,#74458,#74459);
#63155=AXIS2_PLACEMENT_3D('',#105499,#74461,#74462);
#63156=AXIS2_PLACEMENT_3D('',#105506,#74467,#74468);
#63157=AXIS2_PLACEMENT_3D('',#105511,#74472,#74473);
#63158=AXIS2_PLACEMENT_3D('',#105516,#74477,#74478);
#63159=AXIS2_PLACEMENT_3D('',#105517,#74479,#74480);
#63160=AXIS2_PLACEMENT_3D('',#105518,#74481,#74482);
#63161=AXIS2_PLACEMENT_3D('',#105520,#74484,#74485);
#63162=AXIS2_PLACEMENT_3D('',#105521,#74486,#74487);
#63163=AXIS2_PLACEMENT_3D('',#105523,#74489,#74490);
#63164=AXIS2_PLACEMENT_3D('',#105525,#74492,#74493);
#63165=AXIS2_PLACEMENT_3D('',#105528,#74495,#74496);
#63166=AXIS2_PLACEMENT_3D('',#105529,#74497,#74498);
#63167=AXIS2_PLACEMENT_3D('',#105530,#74499,#74500);
#63168=AXIS2_PLACEMENT_3D('',#105531,#74501,#74502);
#63169=AXIS2_PLACEMENT_3D('',#105532,#74503,#74504);
#63170=AXIS2_PLACEMENT_3D('',#105533,#74505,#74506);
#63171=AXIS2_PLACEMENT_3D('',#105534,#74507,#74508);
#63172=AXIS2_PLACEMENT_3D('',#105535,#74509,#74510);
#63173=AXIS2_PLACEMENT_3D('',#105538,#74512,#74513);
#63174=AXIS2_PLACEMENT_3D('',#105539,#74514,#74515);
#63175=AXIS2_PLACEMENT_3D('',#105541,#74517,#74518);
#63176=AXIS2_PLACEMENT_3D('',#105542,#74519,#74520);
#63177=AXIS2_PLACEMENT_3D('',#105545,#74522,#74523);
#63178=AXIS2_PLACEMENT_3D('',#105547,#74525,#74526);
#63179=AXIS2_PLACEMENT_3D('',#105549,#74528,#74529);
#63180=AXIS2_PLACEMENT_3D('',#105550,#74530,#74531);
#63181=AXIS2_PLACEMENT_3D('',#105552,#74532,#74533);
#63182=AXIS2_PLACEMENT_3D('',#105553,#74534,#74535);
#63183=AXIS2_PLACEMENT_3D('',#105555,#74537,#74538);
#63184=AXIS2_PLACEMENT_3D('',#105556,#74539,#74540);
#63185=AXIS2_PLACEMENT_3D('',#105557,#74541,#74542);
#63186=AXIS2_PLACEMENT_3D('',#105559,#74543,#74544);
#63187=AXIS2_PLACEMENT_3D('',#105561,#74546,#74547);
#74359=DIRECTION('axis',(0.,0.,1.));
#74360=DIRECTION('refdir',(1.,0.,0.));
#74361=DIRECTION('center_axis',(0.,-1.,0.));
#74362=DIRECTION('ref_axis',(1.,0.,0.));
#74363=DIRECTION('',(0.,1.,0.));
#74364=DIRECTION('center_axis',(0.,-1.,0.));
#74365=DIRECTION('ref_axis',(1.,0.,0.));
#74366=DIRECTION('center_axis',(0.,-1.,0.));
#74367=DIRECTION('ref_axis',(1.,0.,0.));
#74368=DIRECTION('',(0.,1.,0.));
#74369=DIRECTION('center_axis',(0.,-1.,0.));
#74370=DIRECTION('ref_axis',(1.,0.,0.));
#74371=DIRECTION('',(0.,1.,0.));
#74372=DIRECTION('center_axis',(0.,-1.,0.));
#74373=DIRECTION('ref_axis',(1.,0.,0.));
#74374=DIRECTION('',(0.,1.,0.));
#74375=DIRECTION('center_axis',(0.,-1.,0.));
#74376=DIRECTION('ref_axis',(1.,0.,0.));
#74377=DIRECTION('',(0.,1.,0.));
#74378=DIRECTION('center_axis',(0.,-1.,0.));
#74379=DIRECTION('ref_axis',(0.945756964993923,0.,-0.324874996214674));
#74380=DIRECTION('',(0.,-1.,0.));
#74381=DIRECTION('center_axis',(0.,-1.,0.));
#74382=DIRECTION('ref_axis',(1.,0.,-7.54131538696774E-15));
#74383=DIRECTION('center_axis',(0.,-1.,0.));
#74384=DIRECTION('ref_axis',(1.,0.,-7.54131538696774E-15));
#74385=DIRECTION('',(0.,-1.,0.));
#74386=DIRECTION('center_axis',(0.,-1.,0.));
#74387=DIRECTION('ref_axis',(1.,0.,-7.54131538696774E-15));
#74388=DIRECTION('',(0.,-1.,0.));
#74389=DIRECTION('center_axis',(0.,-1.,0.));
#74390=DIRECTION('ref_axis',(1.,0.,-7.54131538696774E-15));
#74391=DIRECTION('',(0.,-1.,0.));
#74392=DIRECTION('center_axis',(0.,1.,0.));
#74393=DIRECTION('ref_axis',(0.,0.,1.));
#74394=DIRECTION('center_axis',(0.,1.,0.));
#74395=DIRECTION('ref_axis',(1.,0.,0.));
#74396=DIRECTION('center_axis',(0.,1.,0.));
#74397=DIRECTION('ref_axis',(1.,0.,0.));
#74398=DIRECTION('center_axis',(0.,1.,0.));
#74399=DIRECTION('ref_axis',(0.,0.,1.));
#74400=DIRECTION('center_axis',(0.,-1.,0.));
#74401=DIRECTION('ref_axis',(1.,0.,0.));
#74402=DIRECTION('center_axis',(0.,-1.,0.));
#74403=DIRECTION('ref_axis',(1.,0.,0.));
#74404=DIRECTION('center_axis',(0.,1.,0.));
#74405=DIRECTION('ref_axis',(1.,0.,-7.54131538696774E-15));
#74406=DIRECTION('center_axis',(0.,-1.,0.));
#74407=DIRECTION('ref_axis',(1.,0.,-7.54131538696774E-15));
#74408=DIRECTION('center_axis',(0.,1.,0.));
#74409=DIRECTION('ref_axis',(1.,0.,0.));
#74410=DIRECTION('center_axis',(0.,-1.,0.));
#74411=DIRECTION('ref_axis',(1.,0.,0.));
#74412=DIRECTION('',(0.70710678118654,-0.707106781186555,8.65956056235484E-17));
#74413=DIRECTION('center_axis',(0.,-1.,0.));
#74414=DIRECTION('ref_axis',(1.,0.,0.));
#74415=DIRECTION('center_axis',(0.,-1.,0.));
#74416=DIRECTION('ref_axis',(1.,0.,0.));
#74417=DIRECTION('center_axis',(0.,-1.,0.));
#74418=DIRECTION('ref_axis',(1.,0.,0.));
#74419=DIRECTION('center_axis',(0.,-1.,0.));
#74420=DIRECTION('ref_axis',(1.,0.,0.));
#74421=DIRECTION('center_axis',(0.,-1.,0.));
#74422=DIRECTION('ref_axis',(1.,0.,0.));
#74423=DIRECTION('center_axis',(0.,-1.,0.));
#74424=DIRECTION('ref_axis',(1.,0.,0.));
#74425=DIRECTION('center_axis',(0.,-1.,0.));
#74426=DIRECTION('ref_axis',(1.,0.,0.));
#74427=DIRECTION('',(0.,1.,0.));
#74428=DIRECTION('',(0.,-1.,0.));
#74429=DIRECTION('center_axis',(0.,1.,0.));
#74430=DIRECTION('ref_axis',(1.,0.,0.));
#74431=DIRECTION('center_axis',(0.,-1.,0.));
#74432=DIRECTION('ref_axis',(1.,0.,0.));
#74433=DIRECTION('',(0.,1.,0.));
#74434=DIRECTION('',(0.,-1.,0.));
#74435=DIRECTION('center_axis',(0.,1.,0.));
#74436=DIRECTION('ref_axis',(1.,0.,0.));
#74437=DIRECTION('center_axis',(0.,-1.,0.));
#74438=DIRECTION('ref_axis',(1.,0.,0.));
#74439=DIRECTION('',(0.,-1.,0.));
#74440=DIRECTION('center_axis',(0.,1.,0.));
#74441=DIRECTION('ref_axis',(1.,0.,0.));
#74442=DIRECTION('',(0.,1.,0.));
#74443=DIRECTION('center_axis',(0.,-1.,0.));
#74444=DIRECTION('ref_axis',(1.,0.,0.));
#74445=DIRECTION('',(0.,1.,0.));
#74446=DIRECTION('',(0.,-1.,0.));
#74447=DIRECTION('center_axis',(0.,1.,0.));
#74448=DIRECTION('ref_axis',(1.,0.,0.));
#74449=DIRECTION('center_axis',(0.,-1.,0.));
#74450=DIRECTION('ref_axis',(1.,0.,0.));
#74451=DIRECTION('',(0.,-1.,0.));
#74452=DIRECTION('center_axis',(0.,1.,0.));
#74453=DIRECTION('ref_axis',(1.,0.,0.));
#74454=DIRECTION('',(0.,1.,0.));
#74455=DIRECTION('center_axis',(0.,-1.,0.));
#74456=DIRECTION('ref_axis',(1.,0.,0.));
#74457=DIRECTION('',(0.,-1.,0.));
#74458=DIRECTION('center_axis',(0.,1.,0.));
#74459=DIRECTION('ref_axis',(1.,0.,0.));
#74460=DIRECTION('',(0.,1.,0.));
#74461=DIRECTION('center_axis',(0.86602540378444,0.,0.499999999999997));
#74462=DIRECTION('ref_axis',(-0.499999999999997,0.,0.86602540378444));
#74463=DIRECTION('',(-0.499999999999997,0.,0.86602540378444));
#74464=DIRECTION('',(0.,-1.,0.));
#74465=DIRECTION('',(-0.499999999999997,0.,0.86602540378444));
#74466=DIRECTION('',(0.,-1.,0.));
#74467=DIRECTION('center_axis',(0.86602540378444,0.,-0.499999999999997));
#74468=DIRECTION('ref_axis',(0.499999999999997,0.,0.86602540378444));
#74469=DIRECTION('',(0.499999999999997,0.,0.86602540378444));
#74470=DIRECTION('',(0.,-1.,0.));
#74471=DIRECTION('',(0.499999999999997,0.,0.86602540378444));
#74472=DIRECTION('center_axis',(0.,0.,-1.));
#74473=DIRECTION('ref_axis',(1.,0.,0.));
#74474=DIRECTION('',(1.,0.,0.));
#74475=DIRECTION('',(0.,-1.,0.));
#74476=DIRECTION('',(1.,0.,0.));
#74477=DIRECTION('center_axis',(0.,1.,0.));
#74478=DIRECTION('ref_axis',(0.,0.,1.));
#74479=DIRECTION('center_axis',(0.,1.,0.));
#74480=DIRECTION('ref_axis',(0.,0.,1.));
#74481=DIRECTION('center_axis',(0.,1.,0.));
#74482=DIRECTION('ref_axis',(0.,0.,1.));
#74483=DIRECTION('',(0.499999999999997,0.,-0.86602540378444));
#74484=DIRECTION('center_axis',(0.,1.,0.));
#74485=DIRECTION('ref_axis',(0.,0.,1.));
#74486=DIRECTION('center_axis',(0.,1.,0.));
#74487=DIRECTION('ref_axis',(0.,0.,1.));
#74488=DIRECTION('',(-0.499999999999997,0.,-0.86602540378444));
#74489=DIRECTION('center_axis',(0.,1.,0.));
#74490=DIRECTION('ref_axis',(0.,0.,1.));
#74491=DIRECTION('',(-1.,0.,0.));
#74492=DIRECTION('center_axis',(0.,1.,0.));
#74493=DIRECTION('ref_axis',(0.,0.,1.));
#74494=DIRECTION('',(0.499999999999997,0.,-0.86602540378444));
#74495=DIRECTION('center_axis',(0.,-1.,0.));
#74496=DIRECTION('ref_axis',(1.,0.,0.));
#74497=DIRECTION('center_axis',(0.,1.,0.));
#74498=DIRECTION('ref_axis',(0.,0.,1.));
#74499=DIRECTION('center_axis',(0.,-1.,0.));
#74500=DIRECTION('ref_axis',(1.,0.,0.));
#74501=DIRECTION('center_axis',(0.,1.,0.));
#74502=DIRECTION('ref_axis',(0.,0.,1.));
#74503=DIRECTION('center_axis',(0.,-1.,0.));
#74504=DIRECTION('ref_axis',(1.,0.,0.));
#74505=DIRECTION('center_axis',(0.,1.,0.));
#74506=DIRECTION('ref_axis',(0.,0.,1.));
#74507=DIRECTION('center_axis',(0.,-1.,0.));
#74508=DIRECTION('ref_axis',(1.,0.,0.));
#74509=DIRECTION('center_axis',(0.,1.,0.));
#74510=DIRECTION('ref_axis',(0.,0.,1.));
#74511=DIRECTION('',(-1.,0.,0.));
#74512=DIRECTION('center_axis',(0.,-1.,0.));
#74513=DIRECTION('ref_axis',(1.,0.,0.));
#74514=DIRECTION('center_axis',(0.,1.,0.));
#74515=DIRECTION('ref_axis',(0.,0.,1.));
#74516=DIRECTION('',(-0.499999999999997,0.,-0.86602540378444));
#74517=DIRECTION('center_axis',(0.,-1.,0.));
#74518=DIRECTION('ref_axis',(1.,0.,0.));
#74519=DIRECTION('center_axis',(0.,1.,0.));
#74520=DIRECTION('ref_axis',(1.,0.,0.));
#74521=DIRECTION('',(0.857167300702111,-0.515038074910056,1.04972719113862E-16));
#74522=DIRECTION('center_axis',(-0.86602540378444,0.,-0.499999999999997));
#74523=DIRECTION('ref_axis',(0.499999999999997,0.,-0.86602540378444));
#74524=DIRECTION('',(0.,-1.,0.));
#74525=DIRECTION('center_axis',(-0.86602540378444,0.,0.499999999999997));
#74526=DIRECTION('ref_axis',(-0.499999999999997,0.,-0.86602540378444));
#74527=DIRECTION('',(0.,-1.,0.));
#74528=DIRECTION('center_axis',(0.,0.,1.));
#74529=DIRECTION('ref_axis',(-1.,0.,0.));
#74530=DIRECTION('center_axis',(0.,1.,0.));
#74531=DIRECTION('ref_axis',(0.,0.,1.));
#74532=DIRECTION('center_axis',(0.,-1.,0.));
#74533=DIRECTION('ref_axis',(1.,0.,0.));
#74534=DIRECTION('center_axis',(0.,-1.,0.));
#74535=DIRECTION('ref_axis',(1.,0.,0.));
#74536=DIRECTION('',(0.707106781186537,0.707106781186558,8.6595605623548E-17));
#74537=DIRECTION('center_axis',(0.,-1.,0.));
#74538=DIRECTION('ref_axis',(1.,0.,0.));
#74539=DIRECTION('center_axis',(0.,1.,0.));
#74540=DIRECTION('ref_axis',(1.,0.,0.));
#74541=DIRECTION('center_axis',(0.,1.,0.));
#74542=DIRECTION('ref_axis',(1.,0.,0.));
#74543=DIRECTION('center_axis',(0.,-1.,0.));
#74544=DIRECTION('ref_axis',(1.,0.,0.));
#74545=DIRECTION('',(-0.707106781186554,0.707106781186541,-8.65956056235501E-17));
#74546=DIRECTION('center_axis',(0.,-1.,0.));
#74547=DIRECTION('ref_axis',(0.,0.,-1.));
#104424=CARTESIAN_POINT('',(0.,0.,0.));
#104425=CARTESIAN_POINT('Origin',(110.,21.8,63.));
#104426=CARTESIAN_POINT('',(108.535151454168,22.7758449541571,63.0010722055425));
#104427=CARTESIAN_POINT('',(108.535593634877,22.8471550458429,63.0009419999783));
#104428=CARTESIAN_POINT('',(108.5365,21.8,63.));
#104429=CARTESIAN_POINT('',(110.634804239707,22.9365,64.3198481804742));
#104430=CARTESIAN_POINT('Ctrl Pts',(108.535151454168,22.7758449541571,63.0010722055425));
#104431=CARTESIAN_POINT('Ctrl Pts',(108.534609827122,22.7795299873345,63.0686757060681));
#104432=CARTESIAN_POINT('Ctrl Pts',(108.538890809892,22.7832150205118,63.1362086042706));
#104433=CARTESIAN_POINT('Ctrl Pts',(108.548231063953,22.7869000536892,63.2030316078625));
#104434=CARTESIAN_POINT('Ctrl Pts',(108.614676337293,22.8131148691669,63.6784011973634));
#104435=CARTESIAN_POINT('Ctrl Pts',(108.937156278306,22.8393296846445,64.1178451327055));
#104436=CARTESIAN_POINT('Ctrl Pts',(109.370783358443,22.8655445001221,64.3239705993014));
#104437=CARTESIAN_POINT('Ctrl Pts',(109.76201538597,22.8891963334148,64.5099434960951));
#104438=CARTESIAN_POINT('Ctrl Pts',(110.243723602036,22.9128481667074,64.5059900849878));
#104439=CARTESIAN_POINT('Ctrl Pts',(110.635601384839,22.9365,64.3206560833115));
#104440=CARTESIAN_POINT('',(109.365992905425,22.9365,64.3190402776368));
#104441=CARTESIAN_POINT('Origin',(110.,22.9365,63.));
#104442=CARTESIAN_POINT('Ctrl Pts',(109.365992905425,22.9365,64.3190402776368));
#104443=CARTESIAN_POINT('Ctrl Pts',(108.931467947367,22.9102851845224,64.1101824354244));
#104444=CARTESIAN_POINT('Ctrl Pts',(108.611923832083,22.8840703690447,63.6711875655686));
#104445=CARTESIAN_POINT('Ctrl Pts',(108.547797686055,22.8578555535671,63.1962282360989));
#104446=CARTESIAN_POINT('Ctrl Pts',(108.53907256493,22.854288717659,63.1316043980001));
#104447=CARTESIAN_POINT('Ctrl Pts',(108.535075951473,22.850721881751,63.0663147562245));
#104448=CARTESIAN_POINT('Ctrl Pts',(108.535593634877,22.8471550458429,63.0009419999783));
#104449=CARTESIAN_POINT('Origin',(110.,21.8,63.));
#104450=CARTESIAN_POINT('',(108.538691682754,22.2758449541571,63.0000133350456));
#104451=CARTESIAN_POINT('',(108.538693030964,22.3471550458429,63.0000503801031));
#104452=CARTESIAN_POINT('',(108.5365,21.8,63.));
#104453=CARTESIAN_POINT('Ctrl Pts',(108.538691682754,22.2758449541571,63.0000133350456));
#104454=CARTESIAN_POINT('Ctrl Pts',(108.538672353139,22.2889077611353,63.2411582590056));
#104455=CARTESIAN_POINT('Ctrl Pts',(108.595183258915,22.3019705681134,63.4822945262169));
#104456=CARTESIAN_POINT('Ctrl Pts',(108.708275285749,22.3150333750916,63.6930719321842));
#104457=CARTESIAN_POINT('Ctrl Pts',(108.935231606881,22.3412481905693,64.1160660722281));
#104458=CARTESIAN_POINT('Ctrl Pts',(109.390060544541,22.3674630060469,64.4167941097764));
#104459=CARTESIAN_POINT('Ctrl Pts',(109.868150657905,22.3936778215245,64.4599709248855));
#104460=CARTESIAN_POINT('Ctrl Pts',(110.346240771269,22.4198926370022,64.5031477399947));
#104461=CARTESIAN_POINT('Ctrl Pts',(110.847592060336,22.4461074524798,64.2887733326647));
#104462=CARTESIAN_POINT('Ctrl Pts',(111.146657814542,22.4723222679575,63.9132814736071));
#104463=CARTESIAN_POINT('Ctrl Pts',(111.445723568747,22.4985370834351,63.5377896145496));
#104464=CARTESIAN_POINT('Ctrl Pts',(111.542503788091,22.5247518989128,63.0011803037645));
#104465=CARTESIAN_POINT('Ctrl Pts',(111.393469204247,22.5509667143904,62.544871616519));
#104466=CARTESIAN_POINT('Ctrl Pts',(111.244434620402,22.5771815298681,62.0885629292735));
#104467=CARTESIAN_POINT('Ctrl Pts',(110.849585233369,22.6033963453457,61.7125548655677));
#104468=CARTESIAN_POINT('Ctrl Pts',(110.386531995343,22.6296111608233,61.5859716219114));
#104469=CARTESIAN_POINT('Ctrl Pts',(109.923478757317,22.655825976301,61.4593883782552));
#104470=CARTESIAN_POINT('Ctrl Pts',(109.392221668298,22.6820407917786,61.5822299546486));
#104471=CARTESIAN_POINT('Ctrl Pts',(109.031798426622,22.7082556072563,61.8992983646752));
#104472=CARTESIAN_POINT('Ctrl Pts',(108.722040107787,22.7307853895566,62.1717962679423));
#104473=CARTESIAN_POINT('Ctrl Pts',(108.538462886891,22.7533151718568,62.5877537695155));
#104474=CARTESIAN_POINT('Ctrl Pts',(108.535151454168,22.7758449541571,63.0010722055425));
#104475=CARTESIAN_POINT('Ctrl Pts',(108.535593634877,22.8471550458429,63.0009419999783));
#104476=CARTESIAN_POINT('Ctrl Pts',(108.538880717169,22.8245070662733,62.5858511782983));
#104477=CARTESIAN_POINT('Ctrl Pts',(108.724172575191,22.8018590867037,62.1674093960939));
#104478=CARTESIAN_POINT('Ctrl Pts',(109.036631363694,22.7792111071341,61.8947847597746));
#104479=CARTESIAN_POINT('Ctrl Pts',(109.398299364136,22.7529962916565,61.5792244020037));
#104480=CARTESIAN_POINT('Ctrl Pts',(109.930343541793,22.7267814761789,61.4590274755454));
#104481=CARTESIAN_POINT('Ctrl Pts',(110.392891232344,22.7005666607012,61.5877509572053));
#104482=CARTESIAN_POINT('Ctrl Pts',(110.855438922895,22.6743518452236,61.7164744388652));
#104483=CARTESIAN_POINT('Ctrl Pts',(111.248490126339,22.6481370297459,62.0941183286433));
#104484=CARTESIAN_POINT('Ctrl Pts',(111.395458055825,22.6219222142683,62.5510554934448));
#104485=CARTESIAN_POINT('Ctrl Pts',(111.542425985311,22.5957073987906,63.0079926582463));
#104486=CARTESIAN_POINT('Ctrl Pts',(111.443310640837,22.569492583313,63.5442230980713));
#104487=CARTESIAN_POINT('Ctrl Pts',(111.142589280421,22.5432777678353,63.9183940558093));
#104488=CARTESIAN_POINT('Ctrl Pts',(110.841867920004,22.5170629523577,64.2925650135474));
#104489=CARTESIAN_POINT('Ctrl Pts',(110.339540543643,22.4908481368801,64.5046764891985));
#104490=CARTESIAN_POINT('Ctrl Pts',(109.861640737496,22.4646333214024,64.4593626824467));
#104491=CARTESIAN_POINT('Ctrl Pts',(109.383740931348,22.4384185059248,64.4140488756948));
#104492=CARTESIAN_POINT('Ctrl Pts',(108.930268695415,22.4122036904471,64.1113097865399));
#104493=CARTESIAN_POINT('Ctrl Pts',(108.705202697107,22.3859888749695,63.6873119495992));
#104494=CARTESIAN_POINT('Ctrl Pts',(108.594067392366,22.3730442652606,63.4779461228103));
#104495=CARTESIAN_POINT('Ctrl Pts',(108.538624017936,22.3600996555518,63.2390139680548));
#104496=CARTESIAN_POINT('Ctrl Pts',(108.538693030964,22.3471550458429,63.0000503801031));
#104497=CARTESIAN_POINT('Origin',(110.,21.8,63.));
#104498=CARTESIAN_POINT('',(108.535165354128,21.7758449541571,62.9989599428665));
#104499=CARTESIAN_POINT('',(108.535223168726,21.8471550458429,62.9989389776376));
#104500=CARTESIAN_POINT('',(108.5365,21.8,63.));
#104501=CARTESIAN_POINT('Ctrl Pts',(108.535165354128,21.7758449541571,62.9989599428665));
#104502=CARTESIAN_POINT('Ctrl Pts',(108.538492774415,21.7982855349361,63.4106834579473));
#104503=CARTESIAN_POINT('Ctrl Pts',(108.720485196504,21.820726115715,63.8249854635966));
#104504=CARTESIAN_POINT('Ctrl Pts',(109.02811348844,21.843166696494,64.0974234057879));
#104505=CARTESIAN_POINT('Ctrl Pts',(109.387481144217,21.8693815119716,64.4156821199451));
#104506=CARTESIAN_POINT('Ctrl Pts',(109.91829942634,21.8955963274493,64.5403441919538));
#104507=CARTESIAN_POINT('Ctrl Pts',(110.381769684567,21.9218111429269,64.4153280294225));
#104508=CARTESIAN_POINT('Ctrl Pts',(110.845239942795,21.9480259584046,64.2903118668911));
#104509=CARTESIAN_POINT('Ctrl Pts',(111.241362177127,21.9742407738822,63.9156174698199));
#104510=CARTESIAN_POINT('Ctrl Pts',(111.391933201201,22.0004555893599,63.4598081819617));
#104511=CARTESIAN_POINT('Ctrl Pts',(111.542504225274,22.0266704048375,63.0039988941035));
#104512=CARTESIAN_POINT('Ctrl Pts',(111.447524039089,22.0528852203152,62.4670747154584));
#104513=CARTESIAN_POINT('Ctrl Pts',(111.149721391282,22.0791000357928,62.0905813507677));
#104514=CARTESIAN_POINT('Ctrl Pts',(110.851918743475,22.1053148512705,61.7140879860771));
#104515=CARTESIAN_POINT('Ctrl Pts',(110.351293634045,22.1315296667481,61.4980254353409));
#104516=CARTESIAN_POINT('Ctrl Pts',(109.873061584462,22.1577444822257,61.5395932303822));
#104517=CARTESIAN_POINT('Ctrl Pts',(109.39482953488,22.1839592977034,61.5811610254236));
#104518=CARTESIAN_POINT('Ctrl Pts',(108.938990545144,22.210174113181,61.8803591662424));
#104519=CARTESIAN_POINT('Ctrl Pts',(108.710612902578,22.2363889286587,62.3025883579216));
#104520=CARTESIAN_POINT('Ctrl Pts',(108.596035529387,22.2495409371582,62.5144213163656));
#104521=CARTESIAN_POINT('Ctrl Pts',(108.538711144364,22.2626929456576,62.7572217133958));
#104522=CARTESIAN_POINT('Ctrl Pts',(108.538691682754,22.2758449541571,63.0000133350456));
#104523=CARTESIAN_POINT('Ctrl Pts',(108.538693030964,22.3471550458429,63.0000503801031));
#104524=CARTESIAN_POINT('Ctrl Pts',(108.538763779879,22.3338848400741,62.7550761356344));
#104525=CARTESIAN_POINT('Ctrl Pts',(108.597174646194,22.3206146343053,62.5100688568027));
#104526=CARTESIAN_POINT('Ctrl Pts',(108.713732195287,22.3073444285366,62.296848641938));
#104527=CARTESIAN_POINT('Ctrl Pts',(108.943987452459,22.2811296130589,61.8756397559441));
#104528=CARTESIAN_POINT('Ctrl Pts',(109.401157727483,22.2549147975813,61.5784785686831));
#104529=CARTESIAN_POINT('Ctrl Pts',(109.879570904104,22.2286999821036,61.5390428883785));
#104530=CARTESIAN_POINT('Ctrl Pts',(110.357984080725,22.202485166626,61.4996072080739));
#104531=CARTESIAN_POINT('Ctrl Pts',(110.857640158943,22.1762703511483,61.7178970347256));
#104532=CARTESIAN_POINT('Ctrl Pts',(111.153761860065,22.1500555356707,62.0957132578734));
#104533=CARTESIAN_POINT('Ctrl Pts',(111.449883561187,22.123840720193,62.4735294810212));
#104534=CARTESIAN_POINT('Ctrl Pts',(111.542470885215,22.0976259047154,63.010872100665));
#104535=CARTESIAN_POINT('Ctrl Pts',(111.389870482629,22.0714110892377,63.4660060388398));
#104536=CARTESIAN_POINT('Ctrl Pts',(111.237270080043,22.0451962737601,63.9211399770146));
#104537=CARTESIAN_POINT('Ctrl Pts',(110.839481950845,22.0189814582824,64.2940652337204));
#104538=CARTESIAN_POINT('Ctrl Pts',(110.37545920875,21.9927666428048,64.4170148824867));
#104539=CARTESIAN_POINT('Ctrl Pts',(109.911436466654,21.9665518273272,64.539964531253));
#104540=CARTESIAN_POINT('Ctrl Pts',(109.381179111661,21.9403370118495,64.4129385720798));
#104541=CARTESIAN_POINT('Ctrl Pts',(109.023233243215,21.9141221963719,64.0930817722642));
#104542=CARTESIAN_POINT('Ctrl Pts',(108.718435944223,21.8917998128622,63.8207179953862));
#104543=CARTESIAN_POINT('Ctrl Pts',(108.53857871652,21.8694774293526,63.4085359193364));
#104544=CARTESIAN_POINT('Ctrl Pts',(108.535223168726,21.8471550458429,62.9989389776376));
#104545=CARTESIAN_POINT('Origin',(110.,21.8,63.));
#104546=CARTESIAN_POINT('',(108.536119189169,21.2758449541571,63.0012553724788));
#104547=CARTESIAN_POINT('',(108.536055248516,21.3471550458429,63.0012487939741));
#104548=CARTESIAN_POINT('',(108.5365,21.8,63.));
#104549=CARTESIAN_POINT('Ctrl Pts',(108.536119189169,21.2758449541571,63.0012553724788));
#104550=CARTESIAN_POINT('Ctrl Pts',(108.535196141184,21.2814484932592,63.1042391566118));
#104551=CARTESIAN_POINT('Ctrl Pts',(108.54515759093,21.2870520323614,63.2070458445866));
#104552=CARTESIAN_POINT('Ctrl Pts',(108.566672435597,21.2926555714635,63.3073748311208));
#104553=CARTESIAN_POINT('Ctrl Pts',(108.667324482937,21.3188703869411,63.7767399628927));
#104554=CARTESIAN_POINT('Ctrl Pts',(109.020835529846,21.3450852024187,64.191877821057));
#104555=CARTESIAN_POINT('Ctrl Pts',(109.468165106858,21.3713000178964,64.3660347715043));
#104556=CARTESIAN_POINT('Ctrl Pts',(109.915494683871,21.397514833374,64.5401917219516));
#104557=CARTESIAN_POINT('Ctrl Pts',(110.456642790987,21.4237296488517,64.4733677646819));
#104558=CARTESIAN_POINT('Ctrl Pts',(110.848166840665,21.4499444643293,64.1956230388321));
#104559=CARTESIAN_POINT('Ctrl Pts',(111.239690890343,21.476159279807,63.9178783129823));
#104560=CARTESIAN_POINT('Ctrl Pts',(111.481590882581,21.5023740952846,63.4292128185525));
#104561=CARTESIAN_POINT('Ctrl Pts',(111.465042009041,21.5285889107623,62.9494629121278));
#104562=CARTESIAN_POINT('Ctrl Pts',(111.4484931355,21.5548037262399,62.4697130057031));
#104563=CARTESIAN_POINT('Ctrl Pts',(111.17349539618,21.5810185417176,61.9988786872835));
#104564=CARTESIAN_POINT('Ctrl Pts',(110.763762457964,21.6072333571952,61.7487733211406));
#104565=CARTESIAN_POINT('Ctrl Pts',(110.354029519748,21.6334481726728,61.4986679549978));
#104566=CARTESIAN_POINT('Ctrl Pts',(109.809561382636,21.6596629881505,61.4692915411317));
#104567=CARTESIAN_POINT('Ctrl Pts',(109.375297068792,21.6858778036281,61.6738598094909));
#104568=CARTESIAN_POINT('Ctrl Pts',(108.941032754949,21.7120926191058,61.87842807785));
#104569=CARTESIAN_POINT('Ctrl Pts',(108.616972264375,21.7383074345834,62.3169410284346));
#104570=CARTESIAN_POINT('Ctrl Pts',(108.548900533804,21.7645222500611,62.7921251818797));
#104571=CARTESIAN_POINT('Ctrl Pts',(108.539100018986,21.7682964847597,62.86053903441));
#104572=CARTESIAN_POINT('Ctrl Pts',(108.534605722217,21.7720707194584,62.9297130195276));
#104573=CARTESIAN_POINT('Ctrl Pts',(108.535165354128,21.7758449541571,62.9989599428665));
#104574=CARTESIAN_POINT('Ctrl Pts',(108.535223168726,21.8471550458429,62.9989389776376));
#104575=CARTESIAN_POINT('Ctrl Pts',(108.534638050138,21.8432626138749,62.9275161284974));
#104576=CARTESIAN_POINT('Ctrl Pts',(108.539419661893,21.8393701819069,62.856171883249));
#104577=CARTESIAN_POINT('Ctrl Pts',(108.549841384691,21.8354777499389,62.7856612678053));
#104578=CARTESIAN_POINT('Ctrl Pts',(108.620029776514,21.8092629344613,62.3107852036201));
#104579=CARTESIAN_POINT('Ctrl Pts',(108.94604094206,21.7830481189837,61.8737207157076));
#104580=CARTESIAN_POINT('Ctrl Pts',(109.381212483832,21.756833303506,61.6710895313997));
#104581=CARTESIAN_POINT('Ctrl Pts',(109.816384025604,21.7306184880284,61.4684583470919));
#104582=CARTESIAN_POINT('Ctrl Pts',(110.360715943603,21.7044036725507,61.5002604663887));
#104583=CARTESIAN_POINT('Ctrl Pts',(110.769330222778,21.6781888570731,61.7521891040544));
#104584=CARTESIAN_POINT('Ctrl Pts',(111.177944501954,21.6519740415954,62.0041177417202));
#104585=CARTESIAN_POINT('Ctrl Pts',(111.450841142307,21.6257592261178,62.4761728977549));
#104586=CARTESIAN_POINT('Ctrl Pts',(111.465252320939,21.5995444106401,62.9559916183289));
#104587=CARTESIAN_POINT('Ctrl Pts',(111.479663499571,21.5733295951625,63.4358103389028));
#104588=CARTESIAN_POINT('Ctrl Pts',(111.235589216481,21.5471147796848,63.923392624016));
#104589=CARTESIAN_POINT('Ctrl Pts',(110.842831074243,21.5208999642072,64.1993901943523));
#104590=CARTESIAN_POINT('Ctrl Pts',(110.450072932004,21.4946851487296,64.4753877646886));
#104591=CARTESIAN_POINT('Ctrl Pts',(109.908630930616,21.4684703332519,64.539800620248));
#104592=CARTESIAN_POINT('Ctrl Pts',(109.46208276499,21.4422555177743,64.3636516574638));
#104593=CARTESIAN_POINT('Ctrl Pts',(109.015534599365,21.4160407022966,64.1875026946796));
#104594=CARTESIAN_POINT('Ctrl Pts',(108.663880269501,21.389825886819,63.7707919135518));
#104595=CARTESIAN_POINT('Ctrl Pts',(108.565318787313,21.3636110713413,63.3009840605131));
#104596=CARTESIAN_POINT('Ctrl Pts',(108.54469520437,21.3581257295085,63.2026787082648));
#104597=CARTESIAN_POINT('Ctrl Pts',(108.535152996528,21.3526403876757,63.102048562661));
#104598=CARTESIAN_POINT('Ctrl Pts',(108.536055248516,21.3471550458429,63.0012487939741));
#104599=CARTESIAN_POINT('Origin',(110.,21.8,63.));
#104600=CARTESIAN_POINT('',(108.538910502742,20.7758449541571,62.9995078540291));
#104601=CARTESIAN_POINT('',(108.538556703894,20.8471550458429,62.999470885696));
#104602=CARTESIAN_POINT('',(108.5365,21.8,63.));
#104603=CARTESIAN_POINT('Ctrl Pts',(108.538910502742,20.7758449541571,62.9995078540291));
#104604=CARTESIAN_POINT('Ctrl Pts',(108.539674695123,20.79082626706,63.2759626459345));
#104605=CARTESIAN_POINT('Ctrl Pts',(108.614868059699,20.8058075799629,63.553027697966));
#104606=CARTESIAN_POINT('Ctrl Pts',(108.761582448019,20.8207888928659,63.7847945943861));
#104607=CARTESIAN_POINT('Ctrl Pts',(109.018308319953,20.8470037083435,64.1903482640043));
#104608=CARTESIAN_POINT('Ctrl Pts',(109.494025855479,20.8732185238212,64.4572025982981));
#104609=CARTESIAN_POINT('Ctrl Pts',(109.974076621128,20.8994333392988,64.465653338363));
#104610=CARTESIAN_POINT('Ctrl Pts',(110.454127386776,20.9256481547764,64.474104078428));
#104611=CARTESIAN_POINT('Ctrl Pts',(110.938511382548,20.9518629702541,64.2241512242641));
#104612=CARTESIAN_POINT('Ctrl Pts',(111.209619270879,20.9780777857317,63.8280556122507));
#104613=CARTESIAN_POINT('Ctrl Pts',(111.48072715921,21.0042926012094,63.4319600002372));
#104614=CARTESIAN_POINT('Ctrl Pts',(111.5385589401,21.030507416687,62.8897216303742));
#104615=CARTESIAN_POINT('Ctrl Pts',(111.356956870685,21.0567222321647,62.445359190286));
#104616=CARTESIAN_POINT('Ctrl Pts',(111.175354801269,21.0829370476423,62.0009967501978));
#104617=CARTESIAN_POINT('Ctrl Pts',(110.754318881549,21.10915186312,61.6545102398845));
#104618=CARTESIAN_POINT('Ctrl Pts',(110.283326143503,21.1353666785976,61.5617338445643));
#104619=CARTESIAN_POINT('Ctrl Pts',(109.812333405456,21.1615814940752,61.4689574492441));
#104620=CARTESIAN_POINT('Ctrl Pts',(109.291383849084,21.1877963095529,61.629891168917));
#104621=CARTESIAN_POINT('Ctrl Pts',(108.954805594784,21.2140111250305,61.9721542314433));
#104622=CARTESIAN_POINT('Ctrl Pts',(108.6901725125,21.234622401406,62.2412569676757));
#104623=CARTESIAN_POINT('Ctrl Pts',(108.539514400086,21.2552336777816,62.6224541901762));
#104624=CARTESIAN_POINT('Ctrl Pts',(108.536119189169,21.2758449541571,63.0012553724788));
#104625=CARTESIAN_POINT('Ctrl Pts',(108.536055248516,21.3471550458429,63.0012487939741));
#104626=CARTESIAN_POINT('Ctrl Pts',(108.539464919121,21.3264255721981,62.6203197266359));
#104627=CARTESIAN_POINT('Ctrl Pts',(108.69203553938,21.3056960985532,62.2369682132769));
#104628=CARTESIAN_POINT('Ctrl Pts',(108.959392687981,21.2849666249084,61.967509145852));
#104629=CARTESIAN_POINT('Ctrl Pts',(109.297496705348,21.2587518094308,61.626747009179));
#104630=CARTESIAN_POINT('Ctrl Pts',(109.819173374592,21.2325369939531,61.4681276607825));
#104631=CARTESIAN_POINT('Ctrl Pts',(110.289739334968,21.2063221784755,61.5630066225246));
#104632=CARTESIAN_POINT('Ctrl Pts',(110.760305295344,21.1801073629978,61.6578855842667));
#104633=CARTESIAN_POINT('Ctrl Pts',(111.179760546851,21.1538925475202,62.0062628561474));
#104634=CARTESIAN_POINT('Ctrl Pts',(111.35939915459,21.1276777320425,62.45141943501));
#104635=CARTESIAN_POINT('Ctrl Pts',(111.539037762329,21.1014629165649,62.8965760138725));
#104636=CARTESIAN_POINT('Ctrl Pts',(111.478859726299,21.0752481010872,63.4385118997171));
#104637=CARTESIAN_POINT('Ctrl Pts',(111.205950097226,21.0490332856096,63.8334159433577));
#104638=CARTESIAN_POINT('Ctrl Pts',(110.933040468152,21.022818470132,64.2283199869983));
#104639=CARTESIAN_POINT('Ctrl Pts',(110.447399246034,20.9966036546543,64.4761921884351));
#104640=CARTESIAN_POINT('Ctrl Pts',(109.967474020253,20.9703888391767,64.465545900025));
#104641=CARTESIAN_POINT('Ctrl Pts',(109.487548794472,20.944174023699,64.4548996116149));
#104642=CARTESIAN_POINT('Ctrl Pts',(109.013339565028,20.9179592082214,64.1857348333581));
#104643=CARTESIAN_POINT('Ctrl Pts',(108.758236669621,20.8917443927437,63.7790903264723));
#104644=CARTESIAN_POINT('Ctrl Pts',(108.613599991322,20.8768812771101,63.5485335127969));
#104645=CARTESIAN_POINT('Ctrl Pts',(108.539397099341,20.8620181614765,63.273782550778));
#104646=CARTESIAN_POINT('Ctrl Pts',(108.538556703894,20.8471550458429,62.999470885696));
#104647=CARTESIAN_POINT('Origin',(110.,23.8608671147362,63.));
#104648=CARTESIAN_POINT('',(108.821943542907,21.1108671147362,63.0010102596085));
#104649=CARTESIAN_POINT('',(108.823905130175,21.0121328852639,62.9995741958514));
#104650=CARTESIAN_POINT('',(108.82225,23.8608671147362,63.));
#104651=CARTESIAN_POINT('',(109.068873933122,20.6635,63.7239975350757));
#104652=CARTESIAN_POINT('Ctrl Pts',(108.821943542907,21.1108671147362,63.0010102596084));
#104653=CARTESIAN_POINT('Ctrl Pts',(108.824675835122,21.0902558383607,62.696170428753));
#104654=CARTESIAN_POINT('Ctrl Pts',(109.100121495157,21.0434297465075,61.9992340416389));
#104655=CARTESIAN_POINT('Ctrl Pts',(110.26820909347,20.9703888391767,61.6383839750614));
#104656=CARTESIAN_POINT('Ctrl Pts',(111.284693660161,20.8917443927437,62.4748878784196));
#104657=CARTESIAN_POINT('Ctrl Pts',(111.145073475788,20.8130999463108,63.7839850566352));
#104658=CARTESIAN_POINT('Ctrl Pts',(110.013761905485,20.7370184820629,64.367766846319));
#104659=CARTESIAN_POINT('Ctrl Pts',(109.284876061192,20.6871518332926,63.997935414755));
#104660=CARTESIAN_POINT('Ctrl Pts',(109.068873933122,20.6635,63.7239975350757));
#104661=CARTESIAN_POINT('',(110.383133178262,20.6635,64.1136893777958));
#104662=CARTESIAN_POINT('Origin',(110.,20.6635,63.));
#104663=CARTESIAN_POINT('Ctrl Pts',(108.823905130175,21.0121328852639,62.9995741958514));
#104664=CARTESIAN_POINT('Ctrl Pts',(108.823388600688,21.0007811854198,62.8309749199433));
#104665=CARTESIAN_POINT('Ctrl Pts',(108.935645570376,20.9632146700981,62.2737067942396));
#104666=CARTESIAN_POINT('Ctrl Pts',(109.786099850077,20.8994333392988,61.6289388285546));
#104667=CARTESIAN_POINT('Ctrl Pts',(111.02805441837,20.8207888928659,62.0667289458579));
#104668=CARTESIAN_POINT('Ctrl Pts',(111.343096451131,20.7421444464329,63.3456128208481));
#104669=CARTESIAN_POINT('Ctrl Pts',(110.750010398298,20.6897148154776,63.9874756972607));
#104670=CARTESIAN_POINT('Ctrl Pts',(110.383133178262,20.6635,64.1136893777958));
#104671=CARTESIAN_POINT('Origin',(110.,23.8608671147362,63.));
#104672=CARTESIAN_POINT('',(108.821175945217,21.6108671147362,62.9991630151766));
#104673=CARTESIAN_POINT('',(108.821892086737,21.5121328852639,63.0010049655641));
#104674=CARTESIAN_POINT('',(108.82225,23.8608671147362,63.));
#104675=CARTESIAN_POINT('Ctrl Pts',(108.821175945217,21.6108671147362,62.9991630151766));
#104676=CARTESIAN_POINT('Ctrl Pts',(108.820725582058,21.6070928800375,62.9434366305081));
#104677=CARTESIAN_POINT('Ctrl Pts',(108.849463542357,21.5771038298612,62.5011162097095));
#104678=CARTESIAN_POINT('Ctrl Pts',(109.40858460534,21.5208999642072,61.7445234309101));
#104679=CARTESIAN_POINT('Ctrl Pts',(110.72306499171,21.4422555177743,61.815445340232));
#104680=CARTESIAN_POINT('Ctrl Pts',(111.38697736783,21.3636110713413,62.9521555251011));
#104681=CARTESIAN_POINT('Ctrl Pts',(110.80297111735,21.2849666249084,64.1319145672564));
#104682=CARTESIAN_POINT('Ctrl Pts',(109.496506102338,21.2063221784755,64.2932440835005));
#104683=CARTESIAN_POINT('Ctrl Pts',(108.866720300925,21.1482890084181,63.553669094296));
#104684=CARTESIAN_POINT('Ctrl Pts',(108.821200721065,21.1164706538383,63.0838863455412));
#104685=CARTESIAN_POINT('Ctrl Pts',(108.821943542907,21.1108671147362,63.0010102596084));
#104686=CARTESIAN_POINT('Ctrl Pts',(108.821892086737,21.5121328852639,63.0010049655641));
#104687=CARTESIAN_POINT('Ctrl Pts',(108.824636015371,21.491403411619,62.694452721589));
#104688=CARTESIAN_POINT('Ctrl Pts',(109.102687866082,21.4444591224965,61.9958149525211));
#104689=CARTESIAN_POINT('Ctrl Pts',(110.274298694314,21.3713000178964,61.6395786914333));
#104690=CARTESIAN_POINT('Ctrl Pts',(111.286967138036,21.2926555714635,62.4806473596071));
#104691=CARTESIAN_POINT('Ctrl Pts',(111.141682515009,21.2140111250305,63.7890142667887));
#104692=CARTESIAN_POINT('Ctrl Pts',(109.969224812209,21.1353666785976,64.3874389034312));
#104693=CARTESIAN_POINT('Ctrl Pts',(108.989617906622,21.0680739320087,63.8314065465111));
#104694=CARTESIAN_POINT('Ctrl Pts',(108.824581437478,21.0269960008975,63.2203262037437));
#104695=CARTESIAN_POINT('Ctrl Pts',(108.823905130175,21.0121328852639,62.9995741958514));
#104696=CARTESIAN_POINT('Origin',(110.,23.8608671147362,63.));
#104697=CARTESIAN_POINT('',(108.824013754263,22.1108671147362,63.0000107313632));
#104698=CARTESIAN_POINT('',(108.82122247145,22.0121328852639,62.999146143432));
#104699=CARTESIAN_POINT('',(108.82225,23.8608671147362,63.));
#104700=CARTESIAN_POINT('Ctrl Pts',(108.824013754263,22.1108671147362,63.0000107313632));
#104701=CARTESIAN_POINT('Ctrl Pts',(108.824029415972,22.0977151062367,62.8046244434246));
#104702=CARTESIAN_POINT('Ctrl Pts',(108.962111740001,22.0583482822596,62.2197696197103));
#104703=CARTESIAN_POINT('Ctrl Pts',(109.879825660995,21.9927666428048,61.6174115390114));
#104704=CARTESIAN_POINT('Ctrl Pts',(111.088458163825,21.9141221963719,62.1390398324099));
#104705=CARTESIAN_POINT('Ctrl Pts',(111.317763761938,21.8354777499389,63.4353072421795));
#104706=CARTESIAN_POINT('Ctrl Pts',(110.361426977206,21.756833303506,64.3399119421809));
#104707=CARTESIAN_POINT('Ctrl Pts',(109.141402582769,21.6819630917717,64.0533905957354));
#104708=CARTESIAN_POINT('Ctrl Pts',(108.823853682998,21.6333076955151,63.33049705678));
#104709=CARTESIAN_POINT('Ctrl Pts',(108.821175945217,21.6108671147362,62.9991630151766));
#104710=CARTESIAN_POINT('Ctrl Pts',(108.82122247145,22.0121328852639,62.999146143432));
#104711=CARTESIAN_POINT('Ctrl Pts',(108.820751597916,22.0082404532959,62.9416686848909));
#104712=CARTESIAN_POINT('Ctrl Pts',(108.850515147101,21.9781332058502,62.4975803603857));
#104713=CARTESIAN_POINT('Ctrl Pts',(109.414184741874,21.9218111429269,61.7419008351798));
#104714=CARTESIAN_POINT('Ctrl Pts',(110.728336261702,21.843166696494,61.8186789957575));
#104715=CARTESIAN_POINT('Ctrl Pts',(111.38717606664,21.7645222500611,62.9583365837722));
#104716=CARTESIAN_POINT('Ctrl Pts',(110.797920541717,21.6858778036281,64.1354804914431));
#104717=CARTESIAN_POINT('Ctrl Pts',(109.49074599344,21.6072333571952,64.2909890134145));
#104718=CARTESIAN_POINT('Ctrl Pts',(108.865543924084,21.5493183844071,63.5501238496472));
#104719=CARTESIAN_POINT('Ctrl Pts',(108.821166000452,21.5176182270967,63.0821234674916));
#104720=CARTESIAN_POINT('Ctrl Pts',(108.821892086737,21.5121328852639,63.0010049655641));
#104721=CARTESIAN_POINT('Origin',(110.,23.8608671147362,63.));
#104722=CARTESIAN_POINT('',(108.821164759239,22.6108671147362,63.0008628562198));
#104723=CARTESIAN_POINT('',(108.824014839234,22.5121328852639,63.0000405433321));
#104724=CARTESIAN_POINT('',(108.82225,23.8608671147362,63.));
#104725=CARTESIAN_POINT('Ctrl Pts',(108.821164759239,22.6108671147362,63.0008628562198));
#104726=CARTESIAN_POINT('Ctrl Pts',(108.823829631046,22.5883373324359,62.668245303756));
#104727=CARTESIAN_POINT('Ctrl Pts',(109.143460468695,22.539592734658,61.9440114145794));
#104728=CARTESIAN_POINT('Ctrl Pts',(110.365948167423,22.4646333214024,61.6613378858167));
#104729=CARTESIAN_POINT('Ctrl Pts',(111.319211984801,22.3859888749695,62.5691141011147));
#104730=CARTESIAN_POINT('Ctrl Pts',(111.085560662631,22.3073444285365,63.8646213422023));
#104731=CARTESIAN_POINT('Ctrl Pts',(109.875174983029,22.2286999821036,64.3821740410055));
#104732=CARTESIAN_POINT('Ctrl Pts',(108.960740012569,22.1632075441702,63.7775594016063));
#104733=CARTESIAN_POINT('Ctrl Pts',(108.823998198777,22.1239299217143,63.1940718411642));
#104734=CARTESIAN_POINT('Ctrl Pts',(108.824013754263,22.1108671147362,63.0000107313632));
#104735=CARTESIAN_POINT('Ctrl Pts',(108.824014839234,22.5121328852639,63.0000405433321));
#104736=CARTESIAN_POINT('Ctrl Pts',(108.824071774344,22.4988626794951,62.8028977921035));
#104737=CARTESIAN_POINT('Ctrl Pts',(108.963936678654,22.4593776582486,62.2162275067456));
#104738=CARTESIAN_POINT('Ctrl Pts',(109.885989617323,22.3936778215245,61.6168920710419));
#104739=CARTESIAN_POINT('Ctrl Pts',(111.092282639778,22.3150333750916,62.1438975579004));
#104740=CARTESIAN_POINT('Ctrl Pts',(111.315811278397,22.2363889286587,63.4411751874573));
#104741=CARTESIAN_POINT('Ctrl Pts',(110.355452612535,22.1577444822257,64.3415087462245));
#104742=CARTESIAN_POINT('Ctrl Pts',(109.138641455968,22.0829924677608,64.0500151858993));
#104743=CARTESIAN_POINT('Ctrl Pts',(108.823922844811,22.0344552687735,63.3287688274674));
#104744=CARTESIAN_POINT('Ctrl Pts',(108.82122247145,22.0121328852639,62.999146143432));
#104745=CARTESIAN_POINT('Origin',(110.,20.6635,63.));
#104746=CARTESIAN_POINT('',(109.768242272559,20.6635,61.5549669187969));
#104747=CARTESIAN_POINT('Ctrl Pts',(109.068873933122,20.6635,63.7239975350756));
#104748=CARTESIAN_POINT('Ctrl Pts',(109.041776223981,20.6635,63.6968600192059));
#104749=CARTESIAN_POINT('Ctrl Pts',(109.016146947533,20.6635,63.6684047525815));
#104750=CARTESIAN_POINT('Ctrl Pts',(108.992115422948,20.6635,63.6387040998972));
#104751=CARTESIAN_POINT('Ctrl Pts',(108.961661304745,20.6635,63.6010657393193));
#104752=CARTESIAN_POINT('Ctrl Pts',(108.933771170535,20.6635,63.5614286691606));
#104753=CARTESIAN_POINT('Ctrl Pts',(108.908428625451,20.6635,63.5200940182358));
#104754=CARTESIAN_POINT('Ctrl Pts',(108.899116069597,20.6635,63.5049048869096));
#104755=CARTESIAN_POINT('Ctrl Pts',(108.890147843561,20.6635,63.4894861345279));
#104756=CARTESIAN_POINT('Ctrl Pts',(108.881524308389,20.6635,63.4738514603582));
#104757=CARTESIAN_POINT('Ctrl Pts',(108.876113389274,20.6635,63.464041335436));
#104758=CARTESIAN_POINT('Ctrl Pts',(108.870840777671,20.6635,63.4541507322455));
#104759=CARTESIAN_POINT('Ctrl Pts',(108.865709654558,20.6635,63.4441901037785));
#104760=CARTESIAN_POINT('Ctrl Pts',(108.842551675354,20.6635,63.3992354180603));
#104761=CARTESIAN_POINT('Ctrl Pts',(108.822250117441,20.6635,63.3528167020419));
#104762=CARTESIAN_POINT('Ctrl Pts',(108.804784889777,20.6635,63.3052653277658));
#104763=CARTESIAN_POINT('Ctrl Pts',(108.792325591787,20.6635,63.2713432539566));
#104764=CARTESIAN_POINT('Ctrl Pts',(108.781310429759,20.6635,63.2368437412891));
#104765=CARTESIAN_POINT('Ctrl Pts',(108.771744228615,20.6635,63.2018765378799));
#104766=CARTESIAN_POINT('Ctrl Pts',(108.768234596496,20.6635,63.1890478278897));
#104767=CARTESIAN_POINT('Ctrl Pts',(108.76492009768,20.6635,63.1761560983945));
#104768=CARTESIAN_POINT('Ctrl Pts',(108.761801339773,20.6635,63.1632065587171));
#104769=CARTESIAN_POINT('Ctrl Pts',(108.759408740941,20.6635,63.1532721378926));
#104770=CARTESIAN_POINT('Ctrl Pts',(108.757133691864,20.6635,63.1433134201745));
#104771=CARTESIAN_POINT('Ctrl Pts',(108.754975905346,20.6635,63.1333330868544));
#104772=CARTESIAN_POINT('Ctrl Pts',(108.743883262358,20.6635,63.0820266793297));
#104773=CARTESIAN_POINT('Ctrl Pts',(108.735886220507,20.6635,63.030151426245));
#104774=CARTESIAN_POINT('Ctrl Pts',(108.730968273879,20.6635,62.9780444433024));
#104775=CARTESIAN_POINT('Ctrl Pts',(108.725962577061,20.6635,62.9250077232215));
#104776=CARTESIAN_POINT('Ctrl Pts',(108.724146366546,20.6635,62.8717298546305));
#104777=CARTESIAN_POINT('Ctrl Pts',(108.725548337084,20.6635,62.8185401910312));
#104778=CARTESIAN_POINT('Ctrl Pts',(108.726365137912,20.6635,62.7875514076506));
#104779=CARTESIAN_POINT('Ctrl Pts',(108.728275190858,20.6635,62.7565921586689));
#104780=CARTESIAN_POINT('Ctrl Pts',(108.731292161217,20.6635,62.7257258953858));
#104781=CARTESIAN_POINT('Ctrl Pts',(108.732846162307,20.6635,62.7098270958947));
#104782=CARTESIAN_POINT('Ctrl Pts',(108.734693943388,20.6635,62.693952958583));
#104783=CARTESIAN_POINT('Ctrl Pts',(108.736838021663,20.6635,62.6781121640002));
#104784=CARTESIAN_POINT('Ctrl Pts',(108.738124124167,20.6635,62.6686102321863));
#104785=CARTESIAN_POINT('Ctrl Pts',(108.739516716316,20.6635,62.6591219348981));
#104786=CARTESIAN_POINT('Ctrl Pts',(108.741014126988,20.6635,62.6496611766502));
#104787=CARTESIAN_POINT('Ctrl Pts',(108.749581424227,20.6635,62.5955323197334));
#104788=CARTESIAN_POINT('Ctrl Pts',(108.761589938658,20.6635,62.5421986312183));
#104789=CARTESIAN_POINT('Ctrl Pts',(108.777050275135,20.6635,62.4900067495456));
#104790=CARTESIAN_POINT('Ctrl Pts',(108.780620366447,20.6635,62.4779546325946));
#104791=CARTESIAN_POINT('Ctrl Pts',(108.784374733632,20.6635,62.46596334393));
#104792=CARTESIAN_POINT('Ctrl Pts',(108.788313895805,20.6635,62.4540370771723));
#104793=CARTESIAN_POINT('Ctrl Pts',(108.804806146037,20.6635,62.4041048918261));
#104794=CARTESIAN_POINT('Ctrl Pts',(108.824533476475,20.6635,62.3553118205143));
#104795=CARTESIAN_POINT('Ctrl Pts',(108.847241455824,20.6635,62.3078108423137));
#104796=CARTESIAN_POINT('Ctrl Pts',(108.858185154999,20.6635,62.2849186065964));
#104797=CARTESIAN_POINT('Ctrl Pts',(108.869821912433,20.6635,62.2623265854079));
#104798=CARTESIAN_POINT('Ctrl Pts',(108.882127306327,20.6635,62.2400529186177));
#104799=CARTESIAN_POINT('Ctrl Pts',(108.889977865108,20.6635,62.2258428305948));
#104800=CARTESIAN_POINT('Ctrl Pts',(108.898100619865,20.6635,62.2117623333824));
#104801=CARTESIAN_POINT('Ctrl Pts',(108.906489735732,20.6635,62.1978163501422));
#104802=CARTESIAN_POINT('Ctrl Pts',(108.911474485511,20.6635,62.1895297514128));
#104803=CARTESIAN_POINT('Ctrl Pts',(108.91655258614,20.6635,62.1812919793157));
#104804=CARTESIAN_POINT('Ctrl Pts',(108.921716096233,20.6635,62.1731141652028));
#104805=CARTESIAN_POINT('Ctrl Pts',(108.950996938535,20.6635,62.1267400357672));
#104806=CARTESIAN_POINT('Ctrl Pts',(108.98307363302,20.6635,62.0822030694366));
#104807=CARTESIAN_POINT('Ctrl Pts',(109.017648867747,20.6635,62.0396614569002));
#104808=CARTESIAN_POINT('Ctrl Pts',(109.052976298894,20.6635,61.9961943365865));
#104809=CARTESIAN_POINT('Ctrl Pts',(109.090912650005,20.6635,61.9548094783859));
#104810=CARTESIAN_POINT('Ctrl Pts',(109.131193500982,20.6635,61.915691025615));
#104811=CARTESIAN_POINT('Ctrl Pts',(109.153761696009,20.6635,61.8937740886615));
#104812=CARTESIAN_POINT('Ctrl Pts',(109.177066737589,20.6635,61.8725689315292));
#104813=CARTESIAN_POINT('Ctrl Pts',(109.20106819572,20.6635,61.8521115596512));
#104814=CARTESIAN_POINT('Ctrl Pts',(109.21741187414,20.6635,61.838181209859));
#104815=CARTESIAN_POINT('Ctrl Pts',(109.234078558871,20.6635,61.8245976553156));
#104816=CARTESIAN_POINT('Ctrl Pts',(109.251056464039,20.6635,61.811373170307));
#104817=CARTESIAN_POINT('Ctrl Pts',(109.262906518497,20.6635,61.8021428874198));
#104818=CARTESIAN_POINT('Ctrl Pts',(109.274913506492,20.6635,61.7930838780324));
#104819=CARTESIAN_POINT('Ctrl Pts',(109.287044553329,20.6635,61.7842211755186));
#104820=CARTESIAN_POINT('Ctrl Pts',(109.334074367695,20.6635,61.7498621247611));
#104821=CARTESIAN_POINT('Ctrl Pts',(109.383026217507,20.6635,61.7184001999552));
#104822=CARTESIAN_POINT('Ctrl Pts',(109.433611071353,20.6635,61.6900214570481));
#104823=CARTESIAN_POINT('Ctrl Pts',(109.486215208434,20.6635,61.6605098707017));
#104824=CARTESIAN_POINT('Ctrl Pts',(109.540585931337,20.6635,61.6343312922889));
#104825=CARTESIAN_POINT('Ctrl Pts',(109.59644465953,20.6635,61.6117317920506));
#104826=CARTESIAN_POINT('Ctrl Pts',(109.648871874635,20.6635,61.5905206241888));
#104827=CARTESIAN_POINT('Ctrl Pts',(109.702610962679,20.6635,61.5724618781725));
#104828=CARTESIAN_POINT('Ctrl Pts',(109.757458309662,20.6635,61.5578017530401));
#104829=CARTESIAN_POINT('Ctrl Pts',(109.761048227392,20.6635,61.5568422053859));
#104830=CARTESIAN_POINT('Ctrl Pts',(109.764642899831,20.6635,61.5558972351112));
#104831=CARTESIAN_POINT('Ctrl Pts',(109.768242272559,20.6635,61.5549669187969));
#104832=CARTESIAN_POINT('',(108.5365,20.6635,63.));
#104833=CARTESIAN_POINT('Origin',(110.,20.6635,63.));
#104834=CARTESIAN_POINT('',(110.984655829999,20.6635,61.9158283453366));
#104835=CARTESIAN_POINT('Origin',(110.,20.6635,63.));
#104836=CARTESIAN_POINT('Ctrl Pts',(110.985650158356,20.6635,61.9152813028828));
#104837=CARTESIAN_POINT('Ctrl Pts',(111.01753748414,20.6635,61.9498143114107));
#104838=CARTESIAN_POINT('Ctrl Pts',(111.047590571521,20.6635,61.985887892205));
#104839=CARTESIAN_POINT('Ctrl Pts',(111.07563943333,20.6635,62.0234571627525));
#104840=CARTESIAN_POINT('Ctrl Pts',(111.109740975853,20.6635,62.069133528726));
#104841=CARTESIAN_POINT('Ctrl Pts',(111.140881244931,20.6635,62.117021111467));
#104842=CARTESIAN_POINT('Ctrl Pts',(111.169005155357,20.6635,62.1667916134042));
#104843=CARTESIAN_POINT('Ctrl Pts',(111.180163381995,20.6635,62.1865381753901));
#104844=CARTESIAN_POINT('Ctrl Pts',(111.190846276038,20.6635,62.2065812716683));
#104845=CARTESIAN_POINT('Ctrl Pts',(111.201048327816,20.6635,62.2269007098618));
#104846=CARTESIAN_POINT('Ctrl Pts',(111.206203924178,20.6635,62.2371691170324));
#104847=CARTESIAN_POINT('Ctrl Pts',(111.211235029523,20.6635,62.2475049057826));
#104848=CARTESIAN_POINT('Ctrl Pts',(111.216137759321,20.6635,62.2578978974652));
#104849=CARTESIAN_POINT('Ctrl Pts',(111.240666969565,20.6635,62.309895843215));
#104850=CARTESIAN_POINT('Ctrl Pts',(111.262014626778,20.6635,62.3633797304262));
#104851=CARTESIAN_POINT('Ctrl Pts',(111.280130648338,20.6635,62.4180079217357));
#104852=CARTESIAN_POINT('Ctrl Pts',(111.292319973414,20.6635,62.4547643795463));
#104853=CARTESIAN_POINT('Ctrl Pts',(111.303045197808,20.6635,62.4920392539845));
#104854=CARTESIAN_POINT('Ctrl Pts',(111.312277796759,20.6635,62.5297289224477));
#104855=CARTESIAN_POINT('Ctrl Pts',(111.316855469064,20.6635,62.5484160713672));
#104856=CARTESIAN_POINT('Ctrl Pts',(111.321066037847,20.6635,62.5672051745102));
#104857=CARTESIAN_POINT('Ctrl Pts',(111.324905042817,20.6635,62.5860834048704));
#104858=CARTESIAN_POINT('Ctrl Pts',(111.327193300271,20.6635,62.5973358652554));
#104859=CARTESIAN_POINT('Ctrl Pts',(111.329348014919,20.6635,62.6086127768341));
#104860=CARTESIAN_POINT('Ctrl Pts',(111.331367617159,20.6635,62.6199046362027));
#104861=CARTESIAN_POINT('Ctrl Pts',(111.341260805276,20.6635,62.6752187404727));
#104862=CARTESIAN_POINT('Ctrl Pts',(111.347926440227,20.6635,62.7309425734807));
#104863=CARTESIAN_POINT('Ctrl Pts',(111.351312093896,20.6635,62.7867588839852));
#104864=CARTESIAN_POINT('Ctrl Pts',(111.35461246061,20.6635,62.841169143064));
#104865=CARTESIAN_POINT('Ctrl Pts',(111.354795821637,20.6635,62.8956683041584));
#104866=CARTESIAN_POINT('Ctrl Pts',(111.351765888959,20.6635,62.9499533707069));
#104867=CARTESIAN_POINT('Ctrl Pts',(111.349967907017,20.6635,62.9821664855527));
#104868=CARTESIAN_POINT('Ctrl Pts',(111.347037527234,20.6635,63.0143039622647));
#104869=CARTESIAN_POINT('Ctrl Pts',(111.342946754139,20.6635,63.0462987518364));
#104870=CARTESIAN_POINT('Ctrl Pts',(111.340744516677,20.6635,63.0635229103341));
#104871=CARTESIAN_POINT('Ctrl Pts',(111.338205881635,20.6635,63.08070565807));
#104872=CARTESIAN_POINT('Ctrl Pts',(111.335325774837,20.6635,63.0978360597344));
#104873=CARTESIAN_POINT('Ctrl Pts',(111.33322107784,20.6635,63.1103544514009));
#104874=CARTESIAN_POINT('Ctrl Pts',(111.330933144632,20.6635,63.122848499884));
#104875=CARTESIAN_POINT('Ctrl Pts',(111.328465426181,20.6635,63.1352879085258));
#104876=CARTESIAN_POINT('Ctrl Pts',(111.318197868588,20.6635,63.1870451682013));
#104877=CARTESIAN_POINT('Ctrl Pts',(111.304808954063,20.6635,63.2379451290125));
#104878=CARTESIAN_POINT('Ctrl Pts',(111.288220844963,20.6635,63.287708390006));
#104879=CARTESIAN_POINT('Ctrl Pts',(111.283849056323,20.6635,63.3008234749018));
#104880=CARTESIAN_POINT('Ctrl Pts',(111.27925480147,20.6635,63.3138594947431));
#104881=CARTESIAN_POINT('Ctrl Pts',(111.274436108329,20.6635,63.3268110592629));
#104882=CARTESIAN_POINT('Ctrl Pts',(111.256199056831,20.6635,63.3758281562749));
#104883=CARTESIAN_POINT('Ctrl Pts',(111.234749877029,20.6635,63.4236380914674));
#104884=CARTESIAN_POINT('Ctrl Pts',(111.210305646014,20.6635,63.4700291885761));
#104885=CARTESIAN_POINT('Ctrl Pts',(111.198884231714,20.6635,63.4917051390112));
#104886=CARTESIAN_POINT('Ctrl Pts',(111.186808460553,20.6635,63.5130708662858));
#104887=CARTESIAN_POINT('Ctrl Pts',(111.174098316205,20.6635,63.534102023797));
#104888=CARTESIAN_POINT('Ctrl Pts',(111.165070142502,20.6635,63.5490407166999));
#104889=CARTESIAN_POINT('Ctrl Pts',(111.155721872651,20.6635,63.5638105668429));
#104890=CARTESIAN_POINT('Ctrl Pts',(111.146060360571,20.6635,63.5784022275922));
#104891=CARTESIAN_POINT('Ctrl Pts',(111.140434667663,20.6635,63.586898641168));
#104892=CARTESIAN_POINT('Ctrl Pts',(111.134707479,20.6635,63.5953274435488));
#104893=CARTESIAN_POINT('Ctrl Pts',(111.128883474863,20.6635,63.6036831587769));
#104894=CARTESIAN_POINT('Ctrl Pts',(111.098850688879,20.6635,63.6467712818803));
#104895=CARTESIAN_POINT('Ctrl Pts',(111.066222949058,20.6635,63.6879543999203));
#104896=CARTESIAN_POINT('Ctrl Pts',(111.031239521506,20.6635,63.7270332019964));
#104897=CARTESIAN_POINT('Ctrl Pts',(110.996431658519,20.6635,63.765915886844));
#104898=CARTESIAN_POINT('Ctrl Pts',(110.959290675624,20.6635,63.8027159560329));
#104899=CARTESIAN_POINT('Ctrl Pts',(110.920024086437,20.6635,63.8371945338622));
#104900=CARTESIAN_POINT('Ctrl Pts',(110.900351992054,20.6635,63.8544678914741));
#104901=CARTESIAN_POINT('Ctrl Pts',(110.880146046364,20.6635,63.8711578526716));
#104902=CARTESIAN_POINT('Ctrl Pts',(110.859430862329,20.6635,63.8872295854972));
#104903=CARTESIAN_POINT('Ctrl Pts',(110.844179452001,20.6635,63.8990622871329));
#104904=CARTESIAN_POINT('Ctrl Pts',(110.82865198741,20.6635,63.910559808957));
#104905=CARTESIAN_POINT('Ctrl Pts',(110.812858139265,20.6635,63.9217070126001));
#104906=CARTESIAN_POINT('Ctrl Pts',(110.805217406484,20.6635,63.9270997961395));
#104907=CARTESIAN_POINT('Ctrl Pts',(110.797515069741,20.6635,63.9324099343249));
#104908=CARTESIAN_POINT('Ctrl Pts',(110.789763069932,20.6635,63.9376287369471));
#104909=CARTESIAN_POINT('Ctrl Pts',(110.747931937301,20.6635,63.965790299129));
#104910=CARTESIAN_POINT('Ctrl Pts',(110.704574423533,20.6635,63.9913545250727));
#104911=CARTESIAN_POINT('Ctrl Pts',(110.659887444905,20.6635,64.0141163397133));
#104912=CARTESIAN_POINT('Ctrl Pts',(110.616084819746,20.6635,64.0364276989777));
#104913=CARTESIAN_POINT('Ctrl Pts',(110.571003947828,20.6635,64.056046817182));
#104914=CARTESIAN_POINT('Ctrl Pts',(110.524819939819,20.6635,64.0727319238977));
#104915=CARTESIAN_POINT('Ctrl Pts',(110.478635931809,20.6635,64.0894170306134));
#104916=CARTESIAN_POINT('Ctrl Pts',(110.431347991186,20.6635,64.1031686027959));
#104917=CARTESIAN_POINT('Ctrl Pts',(110.383133178262,20.6635,64.1136893777958));
#104918=CARTESIAN_POINT('Ctrl Pts',(109.489783494612,23.1014778394209,64.0614961988294));
#104919=CARTESIAN_POINT('Ctrl Pts',(109.14010001709,23.0752630239433,63.8934180822146));
#104920=CARTESIAN_POINT('Ctrl Pts',(108.625794473154,23.022833392988,63.1868568140592));
#104921=CARTESIAN_POINT('Ctrl Pts',(109.087620120174,22.9441889465551,61.9533607581798));
#104922=CARTESIAN_POINT('Ctrl Pts',(110.372106003814,22.8655445001221,61.6631757288605));
#104923=CARTESIAN_POINT('Ctrl Pts',(111.321028562455,22.7869000536892,62.5749012318044));
#104924=CARTESIAN_POINT('Ctrl Pts',(111.081739672219,22.7082556072563,63.8694937849383));
#104925=CARTESIAN_POINT('Ctrl Pts',(109.868997477121,22.6296111608234,64.381583208474));
#104926=CARTESIAN_POINT('Ctrl Pts',(108.774203642059,22.5509667143904,63.6506963709226));
#104927=CARTESIAN_POINT('Ctrl Pts',(108.782267803706,22.4723222679575,62.3343124775264));
#104928=CARTESIAN_POINT('Ctrl Pts',(109.885989617323,22.3936778215245,61.6168920710419));
#104929=CARTESIAN_POINT('Ctrl Pts',(111.092282639778,22.3150333750916,62.1438975579004));
#104930=CARTESIAN_POINT('Ctrl Pts',(111.315811278397,22.2363889286587,63.4411751874573));
#104931=CARTESIAN_POINT('Ctrl Pts',(110.355452612535,22.1577444822257,64.3415087462245));
#104932=CARTESIAN_POINT('Ctrl Pts',(109.07528055956,22.0791000357928,64.0348367474211));
#104933=CARTESIAN_POINT('Ctrl Pts',(108.627113371416,22.0004555893599,62.7970823192364));
#104934=CARTESIAN_POINT('Ctrl Pts',(109.414184741874,21.9218111429269,61.7419008351798));
#104935=CARTESIAN_POINT('Ctrl Pts',(110.728336261702,21.843166696494,61.8186789957575));
#104936=CARTESIAN_POINT('Ctrl Pts',(111.38717606664,21.7645222500611,62.9583365837722));
#104937=CARTESIAN_POINT('Ctrl Pts',(110.797920541717,21.6858778036281,64.1354804914431));
#104938=CARTESIAN_POINT('Ctrl Pts',(109.49074599344,21.6072333571952,64.2909890134145));
#104939=CARTESIAN_POINT('Ctrl Pts',(108.641765698946,21.5285889107623,63.2849463981635));
#104940=CARTESIAN_POINT('Ctrl Pts',(109.014842533325,21.4499444643293,62.0225249249297));
#104941=CARTESIAN_POINT('Ctrl Pts',(110.274298694314,21.3713000178964,61.6395786914333));
#104942=CARTESIAN_POINT('Ctrl Pts',(111.286967138036,21.2926555714635,62.4806473596071));
#104943=CARTESIAN_POINT('Ctrl Pts',(111.141682515009,21.2140111250305,63.7890142667887));
#104944=CARTESIAN_POINT('Ctrl Pts',(109.969224812209,21.1353666785976,64.3874389034312));
#104945=CARTESIAN_POINT('Ctrl Pts',(108.82436675964,21.0567222321647,63.7376087341273));
#104946=CARTESIAN_POINT('Ctrl Pts',(108.737462181258,20.9780777857317,62.4239586110443));
#104947=CARTESIAN_POINT('Ctrl Pts',(109.786099850077,20.8994333392988,61.6289388285546));
#104948=CARTESIAN_POINT('Ctrl Pts',(111.02805441837,20.8207888928659,62.0667289458579));
#104949=CARTESIAN_POINT('Ctrl Pts',(111.343096451131,20.7421444464329,63.3456128208481));
#104950=CARTESIAN_POINT('Ctrl Pts',(110.750010398298,20.6897148154776,63.9874756972607));
#104951=CARTESIAN_POINT('Ctrl Pts',(110.383133178262,20.6635,64.1136893777958));
#104952=CARTESIAN_POINT('Ctrl Pts',(109.448519964883,23.0464852262806,64.1473442250985));
#104953=CARTESIAN_POINT('Ctrl Pts',(109.070555993849,23.020270410803,63.9656728666179));
#104954=CARTESIAN_POINT('Ctrl Pts',(108.514656221036,22.9678407798477,63.2019687746104));
#104955=CARTESIAN_POINT('Ctrl Pts',(109.013831808942,22.8891963334148,61.8687142816071));
#104956=CARTESIAN_POINT('Ctrl Pts',(110.402199909026,22.8105518869818,61.5550606689361));
#104957=CARTESIAN_POINT('Ctrl Pts',(111.427866151565,22.7319074405489,62.5405215606768));
#104958=CARTESIAN_POINT('Ctrl Pts',(111.169224880268,22.653262994116,63.939813702591));
#104959=CARTESIAN_POINT('Ctrl Pts',(109.858402707175,22.574618547683,64.4933181272659));
#104960=CARTESIAN_POINT('Ctrl Pts',(108.675067914533,22.4959741012501,63.7033211464101));
#104961=CARTESIAN_POINT('Ctrl Pts',(108.683784261615,22.4173296548172,62.2804752994193));
#104962=CARTESIAN_POINT('Ctrl Pts',(109.876769079051,22.3386852083842,61.5050338411687));
#104963=CARTESIAN_POINT('Ctrl Pts',(111.180620505572,22.2600407619513,62.0746606590593));
#104964=CARTESIAN_POINT('Ctrl Pts',(111.422226922012,22.1813963155184,63.4768550317411));
#104965=CARTESIAN_POINT('Ctrl Pts',(110.384199682239,22.1027518690854,64.4500026609583));
#104966=CARTESIAN_POINT('Ctrl Pts',(109.000494291929,22.0241074226525,64.118528702583));
#104967=CARTESIAN_POINT('Ctrl Pts',(108.5160817846,21.9454629762195,62.7806714433351));
#104968=CARTESIAN_POINT('Ctrl Pts',(109.366807197118,21.8668185297866,61.6401526327182));
#104969=CARTESIAN_POINT('Ctrl Pts',(110.787240128335,21.7881740833537,61.7231401924002));
#104970=CARTESIAN_POINT('Ctrl Pts',(111.499363305313,21.7095296369208,62.954967073778));
#104971=CARTESIAN_POINT('Ctrl Pts',(110.862452005608,21.6308851904878,64.2273119640051));
#104972=CARTESIAN_POINT('Ctrl Pts',(109.449560305369,21.5522407440549,64.3953971675455));
#104973=CARTESIAN_POINT('Ctrl Pts',(108.53191911251,21.4735962976219,63.3079913095836));
#104974=CARTESIAN_POINT('Ctrl Pts',(108.935168367584,21.394951851189,61.943472069145));
#104975=CARTESIAN_POINT('Ctrl Pts',(110.296482477488,21.3163074047561,61.5295552317508));
#104976=CARTESIAN_POINT('Ctrl Pts',(111.39105002481,21.2376629583231,62.4386449490808));
#104977=CARTESIAN_POINT('Ctrl Pts',(111.234015573429,21.1590185118902,63.8528254397129));
#104978=CARTESIAN_POINT('Ctrl Pts',(109.966735882778,21.0803740654573,64.4996473989114));
#104979=CARTESIAN_POINT('Ctrl Pts',(108.729287951621,21.0017296190243,63.7972625077853));
#104980=CARTESIAN_POINT('Ctrl Pts',(108.635355004663,20.9230851725914,62.3773715235486));
#104981=CARTESIAN_POINT('Ctrl Pts',(109.768800771936,20.8444407261585,61.5180548747612));
#104982=CARTESIAN_POINT('Ctrl Pts',(111.111197855729,20.7657962797256,61.9912510703265));
#104983=CARTESIAN_POINT('Ctrl Pts',(111.451718770783,20.6871518332926,63.3735641018379));
#104984=CARTESIAN_POINT('Ctrl Pts',(110.810667150952,20.6347222023373,64.067337348854));
#104985=CARTESIAN_POINT('Ctrl Pts',(110.414118901233,20.6085073868597,64.203758503871));
#104986=CARTESIAN_POINT('Ctrl Pts',(109.407256435154,22.9914926131403,64.2331922513677));
#104987=CARTESIAN_POINT('Ctrl Pts',(109.001011970608,22.9652777976627,64.0379276510211));
#104988=CARTESIAN_POINT('Ctrl Pts',(108.403517968918,22.9128481667074,63.2170807351616));
#104989=CARTESIAN_POINT('Ctrl Pts',(108.94004349771,22.8342037202745,61.7840678050346));
#104990=CARTESIAN_POINT('Ctrl Pts',(110.432293814238,22.7555592738415,61.4469456090116));
#104991=CARTESIAN_POINT('Ctrl Pts',(111.534703740675,22.6769148274086,62.5061418895491));
#104992=CARTESIAN_POINT('Ctrl Pts',(111.256710088316,22.5982703809757,64.0101336202436));
#104993=CARTESIAN_POINT('Ctrl Pts',(109.847807937229,22.5196259345427,64.6050530460577));
#104994=CARTESIAN_POINT('Ctrl Pts',(108.575932187007,22.4409814881098,63.7559459218976));
#104995=CARTESIAN_POINT('Ctrl Pts',(108.585300719525,22.3623370416768,62.2266381213122));
#104996=CARTESIAN_POINT('Ctrl Pts',(109.867548540779,22.2836925952439,61.3931756112954));
#104997=CARTESIAN_POINT('Ctrl Pts',(111.268958371366,22.205048148811,62.0054237602183));
#104998=CARTESIAN_POINT('Ctrl Pts',(111.528642565627,22.1264037023781,63.512534876025));
#104999=CARTESIAN_POINT('Ctrl Pts',(110.412946751943,22.0477592559451,64.5584965756923));
#105000=CARTESIAN_POINT('Ctrl Pts',(108.925708024299,21.9691148095122,64.2022206577448));
#105001=CARTESIAN_POINT('Ctrl Pts',(108.405050197784,21.8904703630793,62.7642605674339));
#105002=CARTESIAN_POINT('Ctrl Pts',(109.319429652362,21.8118259166463,61.5384044302566));
#105003=CARTESIAN_POINT('Ctrl Pts',(110.846143994968,21.7331814702134,61.6276013890428));
#105004=CARTESIAN_POINT('Ctrl Pts',(111.611550543987,21.6545370237804,62.9515975637838));
#105005=CARTESIAN_POINT('Ctrl Pts',(110.9269834695,21.5758925773475,64.3191434365672));
#105006=CARTESIAN_POINT('Ctrl Pts',(109.408374617299,21.4972481309146,64.4998053216764));
#105007=CARTESIAN_POINT('Ctrl Pts',(108.422072526074,21.4186036844816,63.3310362210038));
#105008=CARTESIAN_POINT('Ctrl Pts',(108.855494201844,21.3399592380487,61.8644192133603));
#105009=CARTESIAN_POINT('Ctrl Pts',(110.318666260662,21.2613147916158,61.4195317720684));
#105010=CARTESIAN_POINT('Ctrl Pts',(111.495132911584,21.1826703451828,62.3966425385543));
#105011=CARTESIAN_POINT('Ctrl Pts',(111.32634863185,21.1040258987499,63.9166366126373));
#105012=CARTESIAN_POINT('Ctrl Pts',(109.964246953347,21.025381452317,64.6118558943916));
#105013=CARTESIAN_POINT('Ctrl Pts',(108.634209143603,20.946737005884,63.8569162814432));
#105014=CARTESIAN_POINT('Ctrl Pts',(108.533247828067,20.8680925594511,62.3307844360529));
#105015=CARTESIAN_POINT('Ctrl Pts',(109.751501693796,20.7894481130182,61.4071709209678));
#105016=CARTESIAN_POINT('Ctrl Pts',(111.194341293088,20.7108036665852,61.9157731947952));
#105017=CARTESIAN_POINT('Ctrl Pts',(111.560341090435,20.6321592201523,63.4015153828277));
#105018=CARTESIAN_POINT('Ctrl Pts',(110.871323903606,20.579729589197,64.1471990004474));
#105019=CARTESIAN_POINT('Ctrl Pts',(110.445104624204,20.5535147737194,64.2938276299462));
#105020=CARTESIAN_POINT('Ctrl Pts',(109.365992905425,22.9365,64.3190402776368));
#105021=CARTESIAN_POINT('Ctrl Pts',(108.931467947367,22.9102851845224,64.1101824354244));
#105022=CARTESIAN_POINT('Ctrl Pts',(108.2923797168,22.8578555535671,63.2321926957128));
#105023=CARTESIAN_POINT('Ctrl Pts',(108.866255186478,22.7792111071341,61.699421328462));
#105024=CARTESIAN_POINT('Ctrl Pts',(110.46238771945,22.7005666607012,61.3388305490871));
#105025=CARTESIAN_POINT('Ctrl Pts',(111.641541329784,22.6219222142683,62.4717622184214));
#105026=CARTESIAN_POINT('Ctrl Pts',(111.344195296364,22.5432777678353,64.0804535378962));
#105027=CARTESIAN_POINT('Ctrl Pts',(109.837213167282,22.4646333214024,64.7167879648497));
#105028=CARTESIAN_POINT('Ctrl Pts',(108.476796459481,22.3859888749695,63.808570697385));
#105029=CARTESIAN_POINT('Ctrl Pts',(108.486817177434,22.3073444285366,62.1728009432052));
#105030=CARTESIAN_POINT('Ctrl Pts',(109.858328002507,22.2286999821036,61.2813173814221));
#105031=CARTESIAN_POINT('Ctrl Pts',(111.35729623716,22.1500555356707,61.9361868613773));
#105032=CARTESIAN_POINT('Ctrl Pts',(111.635058209242,22.0714110892377,63.5482147203088));
#105033=CARTESIAN_POINT('Ctrl Pts',(110.441693821647,21.9927666428048,64.6669904904262));
#105034=CARTESIAN_POINT('Ctrl Pts',(108.850921756668,21.9141221963719,64.2859126129067));
#105035=CARTESIAN_POINT('Ctrl Pts',(108.294018610968,21.8354777499389,62.7478496915326));
#105036=CARTESIAN_POINT('Ctrl Pts',(109.272052107606,21.756833303506,61.4366562277951));
#105037=CARTESIAN_POINT('Ctrl Pts',(110.905047861601,21.6781888570731,61.5320625856855));
#105038=CARTESIAN_POINT('Ctrl Pts',(111.72373778266,21.5995444106401,62.9482280537896));
#105039=CARTESIAN_POINT('Ctrl Pts',(110.991514933392,21.5208999642072,64.4109749091292));
#105040=CARTESIAN_POINT('Ctrl Pts',(109.367188929228,21.4422555177743,64.6042134758074));
#105041=CARTESIAN_POINT('Ctrl Pts',(108.312225939637,21.3636110713413,63.3540811324239));
#105042=CARTESIAN_POINT('Ctrl Pts',(108.775820036103,21.2849666249084,61.7853663575755));
#105043=CARTESIAN_POINT('Ctrl Pts',(110.340850043836,21.2063221784755,61.309508312386));
#105044=CARTESIAN_POINT('Ctrl Pts',(111.599215798358,21.1276777320425,62.354640128028));
#105045=CARTESIAN_POINT('Ctrl Pts',(111.41868169027,21.0490332856096,63.9804477855616));
#105046=CARTESIAN_POINT('Ctrl Pts',(109.961758023917,20.9703888391767,64.7240643898718));
#105047=CARTESIAN_POINT('Ctrl Pts',(108.539130335584,20.8917443927437,63.9165700551012));
#105048=CARTESIAN_POINT('Ctrl Pts',(108.431140651472,20.8130999463108,62.2841973485573));
#105049=CARTESIAN_POINT('Ctrl Pts',(109.734202615655,20.7344554998779,61.2962869671744));
#105050=CARTESIAN_POINT('Ctrl Pts',(111.277484730447,20.6558110534449,61.8402953192639));
#105051=CARTESIAN_POINT('Ctrl Pts',(111.668963410087,20.577166607012,63.4294666638175));
#105052=CARTESIAN_POINT('Ctrl Pts',(110.93198065626,20.5247369760567,64.2270606520407));
#105053=CARTESIAN_POINT('Ctrl Pts',(110.476090347175,20.4985221605791,64.3838967560213));
#105054=CARTESIAN_POINT('Ctrl Pts',(108.538556703894,20.8471550458429,62.999470885696));
#105055=CARTESIAN_POINT('Ctrl Pts',(108.537914852139,20.8358033459989,62.789965438622));
#105056=CARTESIAN_POINT('Ctrl Pts',(108.580066340676,20.8244516461548,62.5807162394158));
#105057=CARTESIAN_POINT('Ctrl Pts',(108.666315926188,20.8130999463108,62.3916077360841));
#105058=CARTESIAN_POINT('Ctrl Pts',(108.865494639533,20.7868851308332,61.9548938880963));
#105059=CARTESIAN_POINT('Ctrl Pts',(109.299848627594,20.7606703153555,61.6255904276354));
#105060=CARTESIAN_POINT('Ctrl Pts',(109.774239307423,20.7344554998779,61.5516067560865));
#105061=CARTESIAN_POINT('Ctrl Pts',(110.202249540204,20.7108036665852,61.4848563543015));
#105062=CARTESIAN_POINT('Ctrl Pts',(110.662850510825,20.6871518332926,61.6259418135298));
#105063=CARTESIAN_POINT('Ctrl Pts',(110.985650158356,20.6635,61.9152813028828));
#105064=CARTESIAN_POINT('',(109.315335575461,22.9365,62.0417048010816));
#105065=CARTESIAN_POINT('Ctrl Pts',(109.313848625014,22.9365,62.0406439634947));
#105066=CARTESIAN_POINT('Ctrl Pts',(109.280140163402,22.9365,62.0589325036321));
#105067=CARTESIAN_POINT('Ctrl Pts',(109.247463641323,22.9365,62.0789026699033));
#105068=CARTESIAN_POINT('Ctrl Pts',(109.215963639247,22.9365,62.1005219579104));
#105069=CARTESIAN_POINT('Ctrl Pts',(109.17604504973,22.9365,62.1279191460608));
#105070=CARTESIAN_POINT('Ctrl Pts',(109.138014421603,22.9365,62.1579629277155));
#105071=CARTESIAN_POINT('Ctrl Pts',(109.10194186794,22.9365,62.1903599905654));
#105072=CARTESIAN_POINT('Ctrl Pts',(109.088686393136,22.9365,62.202264843611));
#105073=CARTESIAN_POINT('Ctrl Pts',(109.07569551895,22.9365,62.214487933832));
#105074=CARTESIAN_POINT('Ctrl Pts',(109.062973496017,22.9365,62.2270162330653));
#105075=CARTESIAN_POINT('Ctrl Pts',(109.054990947041,22.9365,62.2348772283445));
#105076=CARTESIAN_POINT('Ctrl Pts',(109.047118030534,22.9365,62.2428547839097));
#105077=CARTESIAN_POINT('Ctrl Pts',(109.039360774909,22.9365,62.2509397869167));
#105078=CARTESIAN_POINT('Ctrl Pts',(109.004350387927,22.9365,62.2874293777846));
#105079=CARTESIAN_POINT('Ctrl Pts',(108.971660664562,22.9365,62.3261364097773));
#105080=CARTESIAN_POINT('Ctrl Pts',(108.941366794955,22.9365,62.3667375281165));
#105081=CARTESIAN_POINT('Ctrl Pts',(108.919755827294,22.9365,62.3957014560267));
#105082=CARTESIAN_POINT('Ctrl Pts',(108.899364514413,22.9365,62.4256304788392));
#105083=CARTESIAN_POINT('Ctrl Pts',(108.88022876161,22.9365,62.456420775291));
#105084=CARTESIAN_POINT('Ctrl Pts',(108.873208322306,22.9365,62.4677169813831));
#105085=CARTESIAN_POINT('Ctrl Pts',(108.866356958192,22.9365,62.4791292080189));
#105086=CARTESIAN_POINT('Ctrl Pts',(108.859676736391,22.9365,62.4906526352152));
#105087=CARTESIAN_POINT('Ctrl Pts',(108.854551817076,22.9365,62.4994931552399));
#105088=CARTESIAN_POINT('Ctrl Pts',(108.84953264866,22.9365,62.5083904700141));
#105089=CARTESIAN_POINT('Ctrl Pts',(108.844619720526,22.9365,62.5173419267744));
#105090=CARTESIAN_POINT('Ctrl Pts',(108.819363853716,22.9365,62.5633586389046));
#105091=CARTESIAN_POINT('Ctrl Pts',(108.796913055783,22.9365,62.6108029064586));
#105092=CARTESIAN_POINT('Ctrl Pts',(108.777347590366,22.9365,62.6593468910022));
#105093=CARTESIAN_POINT('Ctrl Pts',(108.757433018356,22.9365,62.7087570458501));
#105094=CARTESIAN_POINT('Ctrl Pts',(108.740506907496,22.9365,62.7593074094981));
#105095=CARTESIAN_POINT('Ctrl Pts',(108.726690634926,22.9365,62.8106904666182));
#105096=CARTESIAN_POINT('Ctrl Pts',(108.718641146458,22.9365,62.8406267119867));
#105097=CARTESIAN_POINT('Ctrl Pts',(108.711647982872,22.9365,62.8708462447828));
#105098=CARTESIAN_POINT('Ctrl Pts',(108.70574232762,22.9365,62.9012921401079));
#105099=CARTESIAN_POINT('Ctrl Pts',(108.702700407335,22.9365,62.9169743942613));
#105100=CARTESIAN_POINT('Ctrl Pts',(108.69994711036,22.9365,62.9327167416041));
#105101=CARTESIAN_POINT('Ctrl Pts',(108.697487323616,22.9365,62.9485115790764));
#105102=CARTESIAN_POINT('Ctrl Pts',(108.696011845669,22.9365,62.9579859509543));
#105103=CARTESIAN_POINT('Ctrl Pts',(108.694642326462,22.9365,62.9674776053876));
#105104=CARTESIAN_POINT('Ctrl Pts',(108.693381127268,22.9365,62.9769727381588));
#105105=CARTESIAN_POINT('Ctrl Pts',(108.686165290403,22.9365,63.0312982796293));
#105106=CARTESIAN_POINT('Ctrl Pts',(108.682474575773,22.9365,63.0858424425533));
#105107=CARTESIAN_POINT('Ctrl Pts',(108.682417947502,22.9365,63.1402759876227));
#105108=CARTESIAN_POINT('Ctrl Pts',(108.682404870894,22.9365,63.1528457892807));
#105109=CARTESIAN_POINT('Ctrl Pts',(108.682585765377,22.9365,63.1654098074689));
#105110=CARTESIAN_POINT('Ctrl Pts',(108.682962323821,22.9365,63.1779641704125));
#105111=CARTESIAN_POINT('Ctrl Pts',(108.684538870899,22.9365,63.2305258499371));
#105112=CARTESIAN_POINT('Ctrl Pts',(108.689540983861,22.9365,63.282917717116));
#105113=CARTESIAN_POINT('Ctrl Pts',(108.697768386234,22.9365,63.3349206222051));
#105114=CARTESIAN_POINT('Ctrl Pts',(108.701733434302,22.9365,63.3599824836571));
#105115=CARTESIAN_POINT('Ctrl Pts',(108.706448361201,22.9365,63.3849541166963));
#105116=CARTESIAN_POINT('Ctrl Pts',(108.711894928251,22.9365,63.4098111733684));
#105117=CARTESIAN_POINT('Ctrl Pts',(108.715369714143,22.9365,63.4256694101346));
#105118=CARTESIAN_POINT('Ctrl Pts',(108.719142342049,22.9365,63.4414810119392));
#105119=CARTESIAN_POINT('Ctrl Pts',(108.723208622296,22.9365,63.4572395968168));
#105120=CARTESIAN_POINT('Ctrl Pts',(108.725624775302,22.9365,63.4666032289071));
#105121=CARTESIAN_POINT('Ctrl Pts',(108.72814432376,22.9365,63.4759466662589));
#105122=CARTESIAN_POINT('Ctrl Pts',(108.730762828323,22.9365,63.4852569757922));
#105123=CARTESIAN_POINT('Ctrl Pts',(108.745611639966,22.9365,63.5380531536391));
#105124=CARTESIAN_POINT('Ctrl Pts',(108.763663964139,22.9365,63.5898852390345));
#105125=CARTESIAN_POINT('Ctrl Pts',(108.784679907723,22.9365,63.6405168651488));
#105126=CARTESIAN_POINT('Ctrl Pts',(108.806153060958,22.9365,63.6922500010769));
#105127=CARTESIAN_POINT('Ctrl Pts',(108.830720405626,22.9365,63.7427308344458));
#105128=CARTESIAN_POINT('Ctrl Pts',(108.85818097311,22.9365,63.7917074971016));
#105129=CARTESIAN_POINT('Ctrl Pts',(108.873566344295,22.9365,63.8191477215167));
#105130=CARTESIAN_POINT('Ctrl Pts',(108.889860870906,22.9365,63.8461157045169));
#105131=CARTESIAN_POINT('Ctrl Pts',(108.907036061991,22.9365,63.8725654110481));
#105132=CARTESIAN_POINT('Ctrl Pts',(108.918731424448,22.9365,63.8905762094857));
#105133=CARTESIAN_POINT('Ctrl Pts',(108.930835239067,22.9365,63.9083466601574));
#105134=CARTESIAN_POINT('Ctrl Pts',(108.943339707194,22.9365,63.9258616387831));
#105135=CARTESIAN_POINT('Ctrl Pts',(108.952067430166,22.9365,63.9380865394941));
#105136=CARTESIAN_POINT('Ctrl Pts',(108.960994393228,22.9365,63.9501920002347));
#105137=CARTESIAN_POINT('Ctrl Pts',(108.970096220285,22.9365,63.9621446561674));
#105138=CARTESIAN_POINT('Ctrl Pts',(109.005382339371,22.9365,64.008482917485));
#105139=CARTESIAN_POINT('Ctrl Pts',(109.043336506866,22.9365,64.0525920408315));
#105140=CARTESIAN_POINT('Ctrl Pts',(109.083734708758,22.9365,64.0942113100944));
#105141=CARTESIAN_POINT('Ctrl Pts',(109.125745560721,22.9365,64.137491973043));
#105142=CARTESIAN_POINT('Ctrl Pts',(109.170399693862,22.9365,64.1780813913725));
#105143=CARTESIAN_POINT('Ctrl Pts',(109.217500216637,22.9365,64.2156643028175));
#105144=CARTESIAN_POINT('Ctrl Pts',(109.261707283157,22.9365,64.2509384392477));
#105145=CARTESIAN_POINT('Ctrl Pts',(109.308070309815,22.9365,64.2835648234591));
#105146=CARTESIAN_POINT('Ctrl Pts',(109.356464298767,22.9365,64.3132494358575));
#105147=CARTESIAN_POINT('Ctrl Pts',(109.359631798921,22.9365,64.3151923634062));
#105148=CARTESIAN_POINT('Ctrl Pts',(109.362808011251,22.9365,64.3171226736369));
#105149=CARTESIAN_POINT('Ctrl Pts',(109.365992905425,22.9365,64.3190402776368));
#105150=CARTESIAN_POINT('Ctrl Pts',(109.313848625014,22.9365,62.0406439634947));
#105151=CARTESIAN_POINT('Ctrl Pts',(109.5989689641,22.9128481667074,61.8396332305574));
#105152=CARTESIAN_POINT('Ctrl Pts',(110.403030903449,22.8629815179371,61.6928883955224));
#105153=CARTESIAN_POINT('Ctrl Pts',(111.321028562455,22.7869000536892,62.5749012318044));
#105154=CARTESIAN_POINT('Ctrl Pts',(111.081739672219,22.7082556072563,63.8694937849383));
#105155=CARTESIAN_POINT('Ctrl Pts',(109.868997477121,22.6296111608234,64.381583208474));
#105156=CARTESIAN_POINT('Ctrl Pts',(108.958935560518,22.5642369201592,63.7740238170161));
#105157=CARTESIAN_POINT('Ctrl Pts',(108.823959301075,22.5250774949727,63.1923462254025));
#105158=CARTESIAN_POINT('Ctrl Pts',(108.824014839234,22.5121328852639,63.0000405433321));
#105159=CARTESIAN_POINT('Origin',(110.,22.9365,63.));
#105160=CARTESIAN_POINT('',(108.5365,22.9365,63.));
#105161=CARTESIAN_POINT('Origin',(110.,22.9365,63.));
#105162=CARTESIAN_POINT('Origin',(110.,22.9365,63.));
#105163=CARTESIAN_POINT('',(110.68466442454,22.9365,62.0417048010816));
#105164=CARTESIAN_POINT('Ctrl Pts',(110.635601384839,22.9365,64.3206560833115));
#105165=CARTESIAN_POINT('Ctrl Pts',(110.676008649758,22.9365,64.29664395265));
#105166=CARTESIAN_POINT('Ctrl Pts',(110.715096848639,22.9365,64.2706323584205));
#105167=CARTESIAN_POINT('Ctrl Pts',(110.75269025251,22.9365,64.2426158721913));
#105168=CARTESIAN_POINT('Ctrl Pts',(110.798395959551,22.9365,64.208553691594));
#105169=CARTESIAN_POINT('Ctrl Pts',(110.841893458597,22.9365,64.171527994697));
#105170=CARTESIAN_POINT('Ctrl Pts',(110.883036378868,22.9365,64.1318377603501));
#105171=CARTESIAN_POINT('Ctrl Pts',(110.899359931227,22.9365,64.1160905646174));
#105172=CARTESIAN_POINT('Ctrl Pts',(110.915312384528,22.9365,64.0999236554903));
#105173=CARTESIAN_POINT('Ctrl Pts',(110.930882702454,22.9365,64.0833548173767));
#105174=CARTESIAN_POINT('Ctrl Pts',(110.938751149424,22.9365,64.0749817690754));
#105175=CARTESIAN_POINT('Ctrl Pts',(110.946519473918,22.9365,64.0665086516793));
#105176=CARTESIAN_POINT('Ctrl Pts',(110.954181051429,22.9365,64.0579441144627));
#105177=CARTESIAN_POINT('Ctrl Pts',(110.992513235231,22.9365,64.0150942686878));
#105178=CARTESIAN_POINT('Ctrl Pts',(111.028219351981,22.9365,63.9699133129342));
#105179=CARTESIAN_POINT('Ctrl Pts',(111.061154023909,22.9365,63.9227144383136));
#105180=CARTESIAN_POINT('Ctrl Pts',(111.083314044193,22.9365,63.8909567811774));
#105181=CARTESIAN_POINT('Ctrl Pts',(111.104218450748,22.9365,63.8582849135692));
#105182=CARTESIAN_POINT('Ctrl Pts',(111.123810367769,22.9365,63.8247900295114));
#105183=CARTESIAN_POINT('Ctrl Pts',(111.133524372102,22.9365,63.8081826986134));
#105184=CARTESIAN_POINT('Ctrl Pts',(111.142915557738,22.9365,63.7913730101249));
#105185=CARTESIAN_POINT('Ctrl Pts',(111.151975993438,22.9365,63.774371987741));
#105186=CARTESIAN_POINT('Ctrl Pts',(111.157376487454,22.9365,63.7642384883516));
#105187=CARTESIAN_POINT('Ctrl Pts',(111.162655947466,22.9365,63.7540434900834));
#105188=CARTESIAN_POINT('Ctrl Pts',(111.167810160439,22.9365,63.7437956545731));
#105189=CARTESIAN_POINT('Ctrl Pts',(111.193058568018,22.9365,63.6935956474827));
#105190=CARTESIAN_POINT('Ctrl Pts',(111.215330076566,22.9365,63.6420829899276));
#105191=CARTESIAN_POINT('Ctrl Pts',(111.234484010569,22.9365,63.5895468299773));
#105192=CARTESIAN_POINT('Ctrl Pts',(111.253155448517,22.9365,63.5383340790941));
#105193=CARTESIAN_POINT('Ctrl Pts',(111.268864506929,22.9365,63.4861477038221));
#105194=CARTESIAN_POINT('Ctrl Pts',(111.281432532302,22.9365,63.4332506881232));
#105195=CARTESIAN_POINT('Ctrl Pts',(111.288890477405,22.9365,63.4018612671534));
#105196=CARTESIAN_POINT('Ctrl Pts',(111.295241437284,22.9365,63.3702215905818));
#105197=CARTESIAN_POINT('Ctrl Pts',(111.300439467589,22.9365,63.3383879468089));
#105198=CARTESIAN_POINT('Ctrl Pts',(111.303237788178,22.9365,63.3212505436816));
#105199=CARTESIAN_POINT('Ctrl Pts',(111.305701862008,22.9365,63.3040569534743));
#105200=CARTESIAN_POINT('Ctrl Pts',(111.307823708633,22.9365,63.2868162116301));
#105201=CARTESIAN_POINT('Ctrl Pts',(111.309374290931,22.9365,63.2742171911429));
#105202=CARTESIAN_POINT('Ctrl Pts',(111.310742299474,22.9365,63.2615892780674));
#105203=CARTESIAN_POINT('Ctrl Pts',(111.311922406986,22.9365,63.2489624959349));
#105204=CARTESIAN_POINT('Ctrl Pts',(111.316832543612,22.9365,63.1964255661834));
#105205=CARTESIAN_POINT('Ctrl Pts',(111.318506445729,22.9365,63.1438207242732));
#105206=CARTESIAN_POINT('Ctrl Pts',(111.316789870112,22.9365,63.0913935960303));
#105207=CARTESIAN_POINT('Ctrl Pts',(111.316337468087,22.9365,63.0775764715292));
#105208=CARTESIAN_POINT('Ctrl Pts',(111.315649293107,22.9365,63.063771725008));
#105209=CARTESIAN_POINT('Ctrl Pts',(111.314721918591,22.9365,63.0499839610383));
#105210=CARTESIAN_POINT('Ctrl Pts',(111.311212128646,22.9365,62.9978020705878));
#105211=CARTESIAN_POINT('Ctrl Pts',(111.304279381792,22.9365,62.945861746428));
#105212=CARTESIAN_POINT('Ctrl Pts',(111.294071418496,22.9365,62.8944277578466));
#105213=CARTESIAN_POINT('Ctrl Pts',(111.289301812052,22.9365,62.870395551204));
#105214=CARTESIAN_POINT('Ctrl Pts',(111.283816571269,22.9365,62.8464741949291));
#105215=CARTESIAN_POINT('Ctrl Pts',(111.27762791159,22.9365,62.8226927216789));
#105216=CARTESIAN_POINT('Ctrl Pts',(111.273232032717,22.9365,62.8058004572379));
#105217=CARTESIAN_POINT('Ctrl Pts',(111.268481212003,22.9365,62.7889787981868));
#105218=CARTESIAN_POINT('Ctrl Pts',(111.263379355067,22.9365,62.772238657017));
#105219=CARTESIAN_POINT('Ctrl Pts',(111.260408650344,22.9365,62.7624912224923));
#105220=CARTESIAN_POINT('Ctrl Pts',(111.257321389305,22.9365,62.7527796664));
#105221=CARTESIAN_POINT('Ctrl Pts',(111.254120497343,22.9365,62.7431105715656));
#105222=CARTESIAN_POINT('Ctrl Pts',(111.237614378183,22.9365,62.6932497098384));
#105223=CARTESIAN_POINT('Ctrl Pts',(111.218077977599,22.9365,62.6444752225303));
#105224=CARTESIAN_POINT('Ctrl Pts',(111.195683828977,22.9365,62.5970463507132));
#105225=CARTESIAN_POINT('Ctrl Pts',(111.173402073509,22.9365,62.5498555178851));
#105226=CARTESIAN_POINT('Ctrl Pts',(111.148290388776,22.9365,62.5039959316499));
#105227=CARTESIAN_POINT('Ctrl Pts',(111.120479595851,22.9365,62.4597557064098));
#105228=CARTESIAN_POINT('Ctrl Pts',(111.106546708327,22.9365,62.4375918621804));
#105229=CARTESIAN_POINT('Ctrl Pts',(111.091935832797,22.9365,62.4158350587755));
#105230=CARTESIAN_POINT('Ctrl Pts',(111.076660633439,22.9365,62.3945256988345));
#105231=CARTESIAN_POINT('Ctrl Pts',(111.065414384295,22.9365,62.3788368449371));
#105232=CARTESIAN_POINT('Ctrl Pts',(111.053807998656,22.9365,62.3633905874213));
#105233=CARTESIAN_POINT('Ctrl Pts',(111.04184643132,22.9365,62.3482041931514));
#105234=CARTESIAN_POINT('Ctrl Pts',(111.03605967185,22.9365,62.34085732895));
#105235=CARTESIAN_POINT('Ctrl Pts',(111.030190308028,22.9365,62.3335721238737));
#105236=CARTESIAN_POINT('Ctrl Pts',(111.024247308606,22.9365,62.3263603111232));
#105237=CARTESIAN_POINT('Ctrl Pts',(110.992177875478,22.9365,62.28744414602));
#105238=CARTESIAN_POINT('Ctrl Pts',(110.957905082491,22.9365,62.2505825372052));
#105239=CARTESIAN_POINT('Ctrl Pts',(110.921559226805,22.9365,62.2160281798043));
#105240=CARTESIAN_POINT('Ctrl Pts',(110.885932624875,22.9365,62.1821576239232));
#105241=CARTESIAN_POINT('Ctrl Pts',(110.848313451306,22.9365,62.1505033205639));
#105242=CARTESIAN_POINT('Ctrl Pts',(110.80880064351,22.9365,62.1213469237875));
#105243=CARTESIAN_POINT('Ctrl Pts',(110.769287835713,22.9365,62.0921905270111));
#105244=CARTESIAN_POINT('Ctrl Pts',(110.727880766146,22.9365,62.0655313526161));
#105245=CARTESIAN_POINT('Ctrl Pts',(110.684664424539,22.9365,62.0417048010816));
#105246=CARTESIAN_POINT('Origin',(110.,22.9365,63.));
#105247=CARTESIAN_POINT('Origin',(110.,23.8608671147362,63.));
#105248=CARTESIAN_POINT('Ctrl Pts',(110.684664424539,22.9365,62.0417048010816));
#105249=CARTESIAN_POINT('Ctrl Pts',(111.000350903699,22.9102851845224,62.2672504386186));
#105250=CARTESIAN_POINT('Ctrl Pts',(111.385893029549,22.8578555535671,63.0515319048078));
#105251=CARTESIAN_POINT('Ctrl Pts',(110.719412413741,22.7792111071341,64.1875760335126));
#105252=CARTESIAN_POINT('Ctrl Pts',(109.404193069561,22.7005666607012,64.2532266483724));
#105253=CARTESIAN_POINT('Ctrl Pts',(108.848682080452,22.6444519965686,63.4962309282256));
#105254=CARTESIAN_POINT('Ctrl Pts',(108.820728885475,22.6145521479135,63.0552666982041));
#105255=CARTESIAN_POINT('Ctrl Pts',(108.821164759239,22.6108671147362,63.0008628562198));
#105256=CARTESIAN_POINT('Ctrl Pts',(110.850780204045,23.1014778394209,61.8091997252243));
#105257=CARTESIAN_POINT('Ctrl Pts',(111.243059688018,23.0752630239433,62.0894680678567));
#105258=CARTESIAN_POINT('Ctrl Pts',(111.722143450431,23.022833392988,63.064034763478));
#105259=CARTESIAN_POINT('Ctrl Pts',(110.893958877104,22.9441889465551,64.4757100615968));
#105260=CARTESIAN_POINT('Ctrl Pts',(109.259636219318,22.8655445001222,64.5572890680476));
#105261=CARTESIAN_POINT('Ctrl Pts',(108.29219639628,22.7869000536892,63.2389572620213));
#105262=CARTESIAN_POINT('Ctrl Pts',(108.860964579279,22.7082556072563,61.705071531042));
#105263=CARTESIAN_POINT('Ctrl Pts',(110.454735846337,22.6296111608233,61.3365468018618));
#105264=CARTESIAN_POINT('Ctrl Pts',(111.639284007435,22.5509667143904,62.4645709929793));
#105265=CARTESIAN_POINT('Ctrl Pts',(111.348943349404,22.4723222679575,64.0743989253347));
#105266=CARTESIAN_POINT('Ctrl Pts',(109.844889482201,22.3936778215245,64.7175221473246));
#105267=CARTESIAN_POINT('Ctrl Pts',(108.48040266922,22.3150333750916,63.8153380346798));
#105268=CARTESIAN_POINT('Ctrl Pts',(108.483151555408,22.2363889286587,62.1795573070613));
#105269=CARTESIAN_POINT('Ctrl Pts',(109.850668524615,22.1577444822257,61.2819628846047));
#105270=CARTESIAN_POINT('Ctrl Pts',(111.352543852904,22.0791000357928,61.9301505368133));
#105271=CARTESIAN_POINT('Ctrl Pts',(111.637484411459,22.0004555893599,63.5409230727486));
#105272=CARTESIAN_POINT('Ctrl Pts',(110.449117708462,21.9218111429269,64.6650062639624));
#105273=CARTESIAN_POINT('Ctrl Pts',(108.856662862094,21.843166696494,64.2910200479365));
#105274=CARTESIAN_POINT('Ctrl Pts',(108.292911773801,21.7645222500611,62.7554539790191));
#105275=CARTESIAN_POINT('Ctrl Pts',(109.265093245523,21.6858778036281,61.4399151272655));
#105276=CARTESIAN_POINT('Ctrl Pts',(110.89849765686,21.6072333571952,61.5280443688639));
#105277=CARTESIAN_POINT('Ctrl Pts',(111.72349087482,21.5285889107623,62.9405473241227));
#105278=CARTESIAN_POINT('Ctrl Pts',(110.997790898104,21.4499444643293,64.4065438074122));
#105279=CARTESIAN_POINT('Ctrl Pts',(109.374346576754,21.3713000178964,64.6070156792213));
#105280=CARTESIAN_POINT('Ctrl Pts',(108.313813436029,21.2926555714635,63.3616021047284));
#105281=CARTESIAN_POINT('Ctrl Pts',(108.770434292712,21.2140111250305,61.79082488859));
#105282=CARTESIAN_POINT('Ctrl Pts',(110.333282961828,21.1353666785976,61.3080237295711));
#105283=CARTESIAN_POINT('Ctrl Pts',(111.59639072099,21.0567222321647,62.3474832605112));
#105284=CARTESIAN_POINT('Ctrl Pts',(111.42289537832,20.9780777857317,63.9741983701003));
#105285=CARTESIAN_POINT('Ctrl Pts',(109.969743391005,20.8994333392988,64.7240569325918));
#105286=CARTESIAN_POINT('Ctrl Pts',(108.542590784426,20.8207888928659,63.9234939297106));
#105287=CARTESIAN_POINT('Ctrl Pts',(108.429388159401,20.7421444464329,62.2907349148822));
#105288=CARTESIAN_POINT('Ctrl Pts',(109.29221212424,20.6897148154776,61.6313137282942));
#105289=CARTESIAN_POINT('Ctrl Pts',(109.768242272559,20.6635,61.5549669187969));
#105290=CARTESIAN_POINT('Ctrl Pts',(110.795408277543,23.0464852262806,61.8867014171768));
#105291=CARTESIAN_POINT('Ctrl Pts',(111.162156759912,23.020270410803,62.1487288581107));
#105292=CARTESIAN_POINT('Ctrl Pts',(111.610059976804,22.9678407798477,63.0598671439213));
#105293=CARTESIAN_POINT('Ctrl Pts',(110.83577672265,22.8891963334148,64.3796653855687));
#105294=CARTESIAN_POINT('Ctrl Pts',(109.307821836066,22.8105518869818,64.4559349281559));
#105295=CARTESIAN_POINT('Ctrl Pts',(108.403346579577,22.7319074405489,63.2234050384426));
#105296=CARTESIAN_POINT('Ctrl Pts',(108.935097222821,22.653262994116,61.7893502715054));
#105297=CARTESIAN_POINT('Ctrl Pts',(110.425139953365,22.574618547683,61.4448104965135));
#105298=CARTESIAN_POINT('Ctrl Pts',(111.532593333224,22.4959741012501,62.4994186956911));
#105299=CARTESIAN_POINT('Ctrl Pts',(111.261149120479,22.4173296548172,64.0044730642906));
#105300=CARTESIAN_POINT('Ctrl Pts',(109.854984649144,22.3386852083842,64.6057394452183));
#105301=CARTESIAN_POINT('Ctrl Pts',(108.579303691261,22.2600407619513,63.7622728158186));
#105302=CARTESIAN_POINT('Ctrl Pts',(108.581873669755,22.1813963155184,62.2329547559868));
#105303=CARTESIAN_POINT('Ctrl Pts',(109.860387570075,22.1027518690854,61.3937791027402));
#105304=CARTESIAN_POINT('Ctrl Pts',(111.264515289878,22.0241074226525,61.9997803020122));
#105305=CARTESIAN_POINT('Ctrl Pts',(111.530910861619,21.9454629762196,63.5057177958922));
#105306=CARTESIAN_POINT('Ctrl Pts',(110.41988746471,21.8668185297866,64.5566414900353));
#105307=CARTESIAN_POINT('Ctrl Pts',(108.931075477322,21.7881740833537,64.2069956819877));
#105308=CARTESIAN_POINT('Ctrl Pts',(108.404015397679,21.7095296369207,62.7713699397287));
#105309=CARTESIAN_POINT('Ctrl Pts',(109.312923698796,21.6308851904878,61.5414512284804));
#105310=CARTESIAN_POINT('Ctrl Pts',(110.84002010181,21.5522407440549,61.6238446926533));
#105311=CARTESIAN_POINT('Ctrl Pts',(111.611319705823,21.4735962976219,62.9444167244488));
#105312=CARTESIAN_POINT('Ctrl Pts',(110.932850971186,21.394951851189,64.3150007273602));
#105313=CARTESIAN_POINT('Ctrl Pts',(109.415066418616,21.3163074047561,64.5024251473144));
#105314=CARTESIAN_POINT('Ctrl Pts',(108.423556702321,21.2376629583232,63.3380677005772));
#105315=CARTESIAN_POINT('Ctrl Pts',(108.850458982579,21.1590185118902,61.8695224829609));
#105316=CARTESIAN_POINT('Ctrl Pts',(110.311591672375,21.0803740654573,61.4181438114013));
#105317=CARTESIAN_POINT('Ctrl Pts',(111.492491700714,21.0017296190243,62.3899514664806));
#105318=CARTESIAN_POINT('Ctrl Pts',(111.330288077476,20.9230851725914,63.9107939322786));
#105319=CARTESIAN_POINT('Ctrl Pts',(109.971712603172,20.8444407261585,64.611848922459));
#105320=CARTESIAN_POINT('Ctrl Pts',(108.637444373619,20.7657962797255,63.8633895246509));
#105321=CARTESIAN_POINT('Ctrl Pts',(108.53160939467,20.6871518332926,62.3368965133499));
#105322=CARTESIAN_POINT('Ctrl Pts',(109.338277580452,20.6347222023373,61.7203928997189));
#105323=CARTESIAN_POINT('Ctrl Pts',(109.783325923764,20.6085073868597,61.6490150233303));
#105324=CARTESIAN_POINT('Ctrl Pts',(110.740036351041,22.9914926131403,61.9642031091292));
#105325=CARTESIAN_POINT('Ctrl Pts',(111.081253831805,22.9652777976627,62.2079896483646));
#105326=CARTESIAN_POINT('Ctrl Pts',(111.497976503177,22.9128481667074,63.0556995243645));
#105327=CARTESIAN_POINT('Ctrl Pts',(110.777594568195,22.8342037202745,64.2836207095406));
#105328=CARTESIAN_POINT('Ctrl Pts',(109.356007452813,22.7555592738415,64.3545807882641));
#105329=CARTESIAN_POINT('Ctrl Pts',(108.514496762873,22.6769148274086,63.2078528148638));
#105330=CARTESIAN_POINT('Ctrl Pts',(109.009229866363,22.5982703809757,61.8736290119688));
#105331=CARTESIAN_POINT('Ctrl Pts',(110.395544060394,22.5196259345427,61.5530741911651));
#105332=CARTESIAN_POINT('Ctrl Pts',(111.425902659012,22.4409814881098,62.5342663984029));
#105333=CARTESIAN_POINT('Ctrl Pts',(111.173354891555,22.3623370416769,63.9345472032464));
#105334=CARTESIAN_POINT('Ctrl Pts',(109.865079816086,22.2836925952439,64.4939567431119));
#105335=CARTESIAN_POINT('Ctrl Pts',(108.678204713302,22.205048148811,63.7092075969576));
#105336=CARTESIAN_POINT('Ctrl Pts',(108.680595784103,22.1264037023781,62.2863522049122));
#105337=CARTESIAN_POINT('Ctrl Pts',(109.870106615535,22.0477592559451,61.5055953208758));
#105338=CARTESIAN_POINT('Ctrl Pts',(111.176486726852,21.9691148095122,62.0694100672111));
#105339=CARTESIAN_POINT('Ctrl Pts',(111.424337311778,21.8904703630792,63.4705125190358));
#105340=CARTESIAN_POINT('Ctrl Pts',(110.390657220958,21.8118259166463,64.4482767161081));
#105341=CARTESIAN_POINT('Ctrl Pts',(109.005488092549,21.7331814702134,64.122971316039));
#105342=CARTESIAN_POINT('Ctrl Pts',(108.515119021557,21.6545370237804,62.7872859004382));
#105343=CARTESIAN_POINT('Ctrl Pts',(109.360754152068,21.5758925773475,61.6429873296953));
#105344=CARTESIAN_POINT('Ctrl Pts',(110.78154254676,21.4972481309146,61.7196450164426));
#105345=CARTESIAN_POINT('Ctrl Pts',(111.499148536827,21.4186036844817,62.948286124775));
#105346=CARTESIAN_POINT('Ctrl Pts',(110.867911044268,21.3399592380487,64.2234576473083));
#105347=CARTESIAN_POINT('Ctrl Pts',(109.455786260477,21.2613147916158,64.3978346154074));
#105348=CARTESIAN_POINT('Ctrl Pts',(108.533299968613,21.1826703451828,63.3145332964259));
#105349=CARTESIAN_POINT('Ctrl Pts',(108.930483672445,21.1040258987499,61.9482200773318));
#105350=CARTESIAN_POINT('Ctrl Pts',(110.289900382923,21.025381452317,61.5282638932313));
#105351=CARTESIAN_POINT('Ctrl Pts',(111.388592680437,20.946737005884,62.4324196724501));
#105352=CARTESIAN_POINT('Ctrl Pts',(111.237680776632,20.8680925594511,63.8473894944569));
#105353=CARTESIAN_POINT('Ctrl Pts',(109.973681815339,20.7894481130182,64.4996409123262));
#105354=CARTESIAN_POINT('Ctrl Pts',(108.732297962812,20.7108036665852,63.8032851195911));
#105355=CARTESIAN_POINT('Ctrl Pts',(108.63383062994,20.6321592201523,62.3830581118176));
#105356=CARTESIAN_POINT('Ctrl Pts',(109.384343036664,20.579729589197,61.8094720711435));
#105357=CARTESIAN_POINT('Ctrl Pts',(109.798409574969,20.5535147737194,61.7430631278637));
#105358=CARTESIAN_POINT('Ctrl Pts',(110.684664424539,22.9365,62.0417048010816));
#105359=CARTESIAN_POINT('Ctrl Pts',(111.000350903699,22.9102851845224,62.2672504386186));
#105360=CARTESIAN_POINT('Ctrl Pts',(111.385893029549,22.8578555535671,63.0515319048078));
#105361=CARTESIAN_POINT('Ctrl Pts',(110.719412413741,22.7792111071341,64.1875760335126));
#105362=CARTESIAN_POINT('Ctrl Pts',(109.404193069561,22.7005666607012,64.2532266483724));
#105363=CARTESIAN_POINT('Ctrl Pts',(108.62564694617,22.6219222142683,63.192300591285));
#105364=CARTESIAN_POINT('Ctrl Pts',(109.083362509905,22.5432777678353,61.9579077524323));
#105365=CARTESIAN_POINT('Ctrl Pts',(110.365948167423,22.4646333214024,61.6613378858167));
#105366=CARTESIAN_POINT('Ctrl Pts',(111.319211984801,22.3859888749695,62.5691141011147));
#105367=CARTESIAN_POINT('Ctrl Pts',(111.085560662631,22.3073444285365,63.8646213422023));
#105368=CARTESIAN_POINT('Ctrl Pts',(109.875174983029,22.2286999821036,64.3821740410055));
#105369=CARTESIAN_POINT('Ctrl Pts',(108.777105735343,22.1500555356707,63.6561423780964));
#105370=CARTESIAN_POINT('Ctrl Pts',(108.77931789845,22.0714110892377,62.3397496538377));
#105371=CARTESIAN_POINT('Ctrl Pts',(109.879825660995,21.9927666428048,61.6174115390114));
#105372=CARTESIAN_POINT('Ctrl Pts',(111.088458163825,21.9141221963719,62.1390398324099));
#105373=CARTESIAN_POINT('Ctrl Pts',(111.317763761938,21.8354777499389,63.4353072421795));
#105374=CARTESIAN_POINT('Ctrl Pts',(110.361426977206,21.756833303506,64.3399119421809));
#105375=CARTESIAN_POINT('Ctrl Pts',(109.079900707777,21.6781888570731,64.0389469500903));
#105376=CARTESIAN_POINT('Ctrl Pts',(108.626222645435,21.5995444106401,62.8032018611478));
#105377=CARTESIAN_POINT('Ctrl Pts',(109.40858460534,21.5208999642072,61.7445234309101));
#105378=CARTESIAN_POINT('Ctrl Pts',(110.72306499171,21.4422555177743,61.815445340232));
#105379=CARTESIAN_POINT('Ctrl Pts',(111.38697736783,21.3636110713413,62.9521555251011));
#105380=CARTESIAN_POINT('Ctrl Pts',(110.80297111735,21.2849666249084,64.1319145672564));
#105381=CARTESIAN_POINT('Ctrl Pts',(109.496506102338,21.2063221784755,64.2932440835005));
#105382=CARTESIAN_POINT('Ctrl Pts',(108.643043234905,21.1276777320425,63.2909988922746));
#105383=CARTESIAN_POINT('Ctrl Pts',(109.010508362311,21.0490332856096,62.0269176717027));
#105384=CARTESIAN_POINT('Ctrl Pts',(110.26820909347,20.9703888391767,61.6383839750614));
#105385=CARTESIAN_POINT('Ctrl Pts',(111.284693660161,20.8917443927437,62.4748878784196));
#105386=CARTESIAN_POINT('Ctrl Pts',(111.145073475788,20.8130999463108,63.7839850566352));
#105387=CARTESIAN_POINT('Ctrl Pts',(109.975651027507,20.7344554998779,64.3874329021934));
#105388=CARTESIAN_POINT('Ctrl Pts',(108.827151552004,20.6558110534449,63.7431807145313));
#105389=CARTESIAN_POINT('Ctrl Pts',(108.73605186521,20.577166607012,62.4292197102853));
#105390=CARTESIAN_POINT('Ctrl Pts',(109.430408492876,20.5247369760567,61.8985512425682));
#105391=CARTESIAN_POINT('Ctrl Pts',(109.813493226174,20.4985221605791,61.8371112323971));
#105392=CARTESIAN_POINT('Ctrl Pts',(109.768242272559,20.6635,61.554966918797));
#105393=CARTESIAN_POINT('Ctrl Pts',(109.29221212424,20.6897148154776,61.6313137282943));
#105394=CARTESIAN_POINT('Ctrl Pts',(108.86080014182,20.7159296309553,61.9610243215882));
#105395=CARTESIAN_POINT('Ctrl Pts',(108.663961254782,20.7421444464329,62.3980061207066));
#105396=CARTESIAN_POINT('Ctrl Pts',(108.57961238167,20.7533779490077,62.585260391853));
#105397=CARTESIAN_POINT('Ctrl Pts',(108.538337485068,20.7646114515824,62.7922125631031));
#105398=CARTESIAN_POINT('Ctrl Pts',(108.538910502742,20.7758449541571,62.9995078540291));
#105399=CARTESIAN_POINT('Origin',(110.,23.1,63.));
#105400=CARTESIAN_POINT('',(108.983974596216,23.2,63.));
#105401=CARTESIAN_POINT('Origin',(110.,23.2,63.));
#105402=CARTESIAN_POINT('',(109.133974596216,23.05,63.));
#105403=CARTESIAN_POINT('',(109.083974596216,23.1,63.));
#105404=CARTESIAN_POINT('',(109.189703570316,23.,62.9034745854044));
#105405=CARTESIAN_POINT('Ctrl Pts',(109.189703570316,23.,62.9034745854044));
#105406=CARTESIAN_POINT('Ctrl Pts',(109.162667372368,23.0213072238479,62.9503026538943));
#105407=CARTESIAN_POINT('Ctrl Pts',(109.133974596216,23.05,63.));
#105408=CARTESIAN_POINT('',(109.511258324007,23.,62.3465254145956));
#105409=CARTESIAN_POINT('Origin',(110.,23.,63.));
#105410=CARTESIAN_POINT('',(109.566987298108,23.05,62.25));
#105411=CARTESIAN_POINT('Ctrl Pts',(109.566987298108,23.05,62.25));
#105412=CARTESIAN_POINT('Ctrl Pts',(109.538294521956,23.0213072238479,62.2996973461057));
#105413=CARTESIAN_POINT('Ctrl Pts',(109.511258324007,23.,62.3465254145956));
#105414=CARTESIAN_POINT('',(109.678445246309,23.,62.25));
#105415=CARTESIAN_POINT('Ctrl Pts',(109.678445246309,23.,62.25));
#105416=CARTESIAN_POINT('Ctrl Pts',(109.624372850412,23.0213072238479,62.25));
#105417=CARTESIAN_POINT('Ctrl Pts',(109.566987298108,23.05,62.25));
#105418=CARTESIAN_POINT('',(110.321554753691,23.,62.25));
#105419=CARTESIAN_POINT('Origin',(110.,23.,63.));
#105420=CARTESIAN_POINT('',(110.433012701892,23.05,62.25));
#105421=CARTESIAN_POINT('Ctrl Pts',(110.433012701892,23.05,62.25));
#105422=CARTESIAN_POINT('Ctrl Pts',(110.375627149588,23.0213072238479,62.25));
#105423=CARTESIAN_POINT('Ctrl Pts',(110.321554753691,23.,62.25));
#105424=CARTESIAN_POINT('',(110.488741675993,23.,62.3465254145956));
#105425=CARTESIAN_POINT('Ctrl Pts',(110.488741675993,23.,62.3465254145956));
#105426=CARTESIAN_POINT('Ctrl Pts',(110.461705478044,23.0213072238479,62.2996973461057));
#105427=CARTESIAN_POINT('Ctrl Pts',(110.433012701892,23.05,62.25));
#105428=CARTESIAN_POINT('',(110.810296429684,23.,62.9034745854044));
#105429=CARTESIAN_POINT('Origin',(110.,23.,63.));
#105430=CARTESIAN_POINT('',(110.866025403784,23.05,63.));
#105431=CARTESIAN_POINT('Ctrl Pts',(110.866025403784,23.05,63.));
#105432=CARTESIAN_POINT('Ctrl Pts',(110.837332627632,23.0213072238478,62.9503026538943));
#105433=CARTESIAN_POINT('Ctrl Pts',(110.810296429684,23.,62.9034745854044));
#105434=CARTESIAN_POINT('',(110.810296429684,23.,63.0965254145955));
#105435=CARTESIAN_POINT('Ctrl Pts',(110.810296429684,23.,63.0965254145956));
#105436=CARTESIAN_POINT('Ctrl Pts',(110.837332627632,23.0213072238479,63.0496973461056));
#105437=CARTESIAN_POINT('Ctrl Pts',(110.866025403784,23.05,63.));
#105438=CARTESIAN_POINT('',(110.488741675993,23.,63.6534745854045));
#105439=CARTESIAN_POINT('Origin',(110.,23.,63.));
#105440=CARTESIAN_POINT('',(110.433012701892,23.05,63.75));
#105441=CARTESIAN_POINT('Ctrl Pts',(110.433012701892,23.05,63.75));
#105442=CARTESIAN_POINT('Ctrl Pts',(110.461705478044,23.0213072238479,63.7003026538944));
#105443=CARTESIAN_POINT('Ctrl Pts',(110.488741675993,23.,63.6534745854045));
#105444=CARTESIAN_POINT('',(110.321554753691,23.,63.75));
#105445=CARTESIAN_POINT('Ctrl Pts',(110.321554753691,23.,63.75));
#105446=CARTESIAN_POINT('Ctrl Pts',(110.375627149588,23.0213072238479,63.75));
#105447=CARTESIAN_POINT('Ctrl Pts',(110.433012701892,23.05,63.75));
#105448=CARTESIAN_POINT('',(109.678445246309,23.,63.75));
#105449=CARTESIAN_POINT('Origin',(110.,23.,63.));
#105450=CARTESIAN_POINT('',(109.566987298108,23.05,63.75));
#105451=CARTESIAN_POINT('Ctrl Pts',(109.566987298108,23.05,63.75));
#105452=CARTESIAN_POINT('Ctrl Pts',(109.624372850412,23.0213072238479,63.75));
#105453=CARTESIAN_POINT('Ctrl Pts',(109.678445246309,23.,63.75));
#105454=CARTESIAN_POINT('',(109.511258324007,23.,63.6534745854045));
#105455=CARTESIAN_POINT('Ctrl Pts',(109.511258324007,23.,63.6534745854045));
#105456=CARTESIAN_POINT('Ctrl Pts',(109.538294521956,23.0213072238479,63.7003026538943));
#105457=CARTESIAN_POINT('Ctrl Pts',(109.566987298108,23.05,63.75));
#105458=CARTESIAN_POINT('',(109.189703570316,23.,63.0965254145955));
#105459=CARTESIAN_POINT('Origin',(110.,23.,63.));
#105460=CARTESIAN_POINT('Ctrl Pts',(109.133974596216,23.05,63.));
#105461=CARTESIAN_POINT('Ctrl Pts',(109.162667372368,23.0213072238479,63.0496973461056));
#105462=CARTESIAN_POINT('Ctrl Pts',(109.189703570316,23.,63.0965254145955));
#105463=CARTESIAN_POINT('Origin',(110.,23.1,63.));
#105464=CARTESIAN_POINT('',(110.321554753691,23.2,62.25));
#105465=CARTESIAN_POINT('',(110.321554753691,23.1,62.25));
#105466=CARTESIAN_POINT('',(109.678445246309,23.2,62.25));
#105467=CARTESIAN_POINT('',(109.678445246309,23.1,62.25));
#105468=CARTESIAN_POINT('Origin',(110.,23.2,63.));
#105469=CARTESIAN_POINT('Origin',(110.,23.1,63.));
#105470=CARTESIAN_POINT('',(110.810296429684,23.2,62.9034745854044));
#105471=CARTESIAN_POINT('',(110.810296429684,23.1,62.9034745854044));
#105472=CARTESIAN_POINT('',(110.488741675993,23.2,62.3465254145956));
#105473=CARTESIAN_POINT('',(110.488741675993,23.1,62.3465254145956));
#105474=CARTESIAN_POINT('Origin',(110.,23.2,63.));
#105475=CARTESIAN_POINT('Origin',(110.,23.1,63.));
#105476=CARTESIAN_POINT('',(109.189703570316,23.2,62.9034745854044));
#105477=CARTESIAN_POINT('',(109.189703570316,23.1,62.9034745854044));
#105478=CARTESIAN_POINT('',(109.511258324007,23.2,62.3465254145956));
#105479=CARTESIAN_POINT('Origin',(110.,23.2,63.));
#105480=CARTESIAN_POINT('',(109.511258324007,23.1,62.3465254145956));
#105481=CARTESIAN_POINT('Origin',(110.,23.1,63.));
#105482=CARTESIAN_POINT('',(110.488741675993,23.2,63.6534745854045));
#105483=CARTESIAN_POINT('',(110.488741675993,23.1,63.6534745854045));
#105484=CARTESIAN_POINT('',(110.810296429684,23.2,63.0965254145955));
#105485=CARTESIAN_POINT('',(110.810296429684,23.1,63.0965254145955));
#105486=CARTESIAN_POINT('Origin',(110.,23.2,63.));
#105487=CARTESIAN_POINT('Origin',(110.,23.1,63.));
#105488=CARTESIAN_POINT('',(109.511258324007,23.2,63.6534745854045));
#105489=CARTESIAN_POINT('',(109.511258324007,23.1,63.6534745854045));
#105490=CARTESIAN_POINT('',(109.189703570316,23.2,63.0965254145955));
#105491=CARTESIAN_POINT('Origin',(110.,23.2,63.));
#105492=CARTESIAN_POINT('',(109.189703570316,23.1,63.0965254145955));
#105493=CARTESIAN_POINT('Origin',(110.,23.1,63.));
#105494=CARTESIAN_POINT('',(110.321554753691,23.2,63.75));
#105495=CARTESIAN_POINT('',(110.321554753691,23.1,63.75));
#105496=CARTESIAN_POINT('',(109.678445246309,23.2,63.75));
#105497=CARTESIAN_POINT('Origin',(110.,23.2,63.));
#105498=CARTESIAN_POINT('',(109.678445246309,23.1,63.75));
#105499=CARTESIAN_POINT('Origin',(110.866025403784,23.2,63.));
#105500=CARTESIAN_POINT('',(110.907772228311,23.2,62.9276923788647));
#105501=CARTESIAN_POINT('',(110.866025403784,22.,63.));
#105502=CARTESIAN_POINT('',(110.866025403784,23.2,63.));
#105503=CARTESIAN_POINT('',(110.433012701892,22.,63.75));
#105504=CARTESIAN_POINT('',(110.866025403784,22.,63.));
#105505=CARTESIAN_POINT('',(110.433012701892,23.2,63.75));
#105506=CARTESIAN_POINT('Origin',(110.433012701892,23.2,62.25));
#105507=CARTESIAN_POINT('',(110.691265877365,23.2,62.6973076211353));
#105508=CARTESIAN_POINT('',(110.433012701892,22.,62.25));
#105509=CARTESIAN_POINT('',(110.433012701892,23.2,62.25));
#105510=CARTESIAN_POINT('',(110.433012701892,22.,62.25));
#105511=CARTESIAN_POINT('Origin',(109.566987298108,23.2,62.25));
#105512=CARTESIAN_POINT('',(110.383493649054,23.2,62.25));
#105513=CARTESIAN_POINT('',(109.566987298108,22.,62.25));
#105514=CARTESIAN_POINT('',(109.566987298108,23.2,62.25));
#105515=CARTESIAN_POINT('',(109.566987298108,22.,62.25));
#105516=CARTESIAN_POINT('Origin',(111.2,23.2,63.));
#105517=CARTESIAN_POINT('Origin',(111.2,23.2,63.));
#105518=CARTESIAN_POINT('Origin',(111.2,23.2,63.));
#105519=CARTESIAN_POINT('',(109.392227771689,23.2,62.5526923788647));
#105520=CARTESIAN_POINT('Origin',(111.2,23.2,63.));
#105521=CARTESIAN_POINT('Origin',(111.2,23.2,63.));
#105522=CARTESIAN_POINT('',(109.608734122635,23.2,63.8223076211353));
#105523=CARTESIAN_POINT('Origin',(111.2,23.2,63.));
#105524=CARTESIAN_POINT('',(110.816506350946,23.2,63.75));
#105525=CARTESIAN_POINT('Origin',(110.866025403784,22.,63.));
#105526=CARTESIAN_POINT('',(109.133974596216,22.,63.));
#105527=CARTESIAN_POINT('',(109.133974596216,22.,63.));
#105528=CARTESIAN_POINT('Origin',(110.,22.,63.));
#105529=CARTESIAN_POINT('Origin',(110.866025403784,22.,63.));
#105530=CARTESIAN_POINT('Origin',(110.,22.,63.));
#105531=CARTESIAN_POINT('Origin',(110.866025403784,22.,63.));
#105532=CARTESIAN_POINT('Origin',(110.,22.,63.));
#105533=CARTESIAN_POINT('Origin',(110.866025403784,22.,63.));
#105534=CARTESIAN_POINT('Origin',(110.,22.,63.));
#105535=CARTESIAN_POINT('Origin',(110.866025403784,22.,63.));
#105536=CARTESIAN_POINT('',(109.566987298108,22.,63.75));
#105537=CARTESIAN_POINT('',(110.433012701892,22.,63.75));
#105538=CARTESIAN_POINT('Origin',(110.,22.,63.));
#105539=CARTESIAN_POINT('Origin',(110.866025403784,22.,63.));
#105540=CARTESIAN_POINT('',(109.566987298108,22.,63.75));
#105541=CARTESIAN_POINT('Origin',(110.,22.,63.));
#105542=CARTESIAN_POINT('Origin',(110.,22.,63.));
#105543=CARTESIAN_POINT('',(110.,21.4796394397885,63.));
#105544=CARTESIAN_POINT('',(109.133974596216,22.,63.));
#105545=CARTESIAN_POINT('Origin',(109.133974596216,23.2,63.));
#105546=CARTESIAN_POINT('',(109.133974596216,23.2,63.));
#105547=CARTESIAN_POINT('Origin',(109.566987298108,23.2,63.75));
#105548=CARTESIAN_POINT('',(109.566987298108,23.2,63.75));
#105549=CARTESIAN_POINT('Origin',(110.433012701892,23.2,63.75));
#105550=CARTESIAN_POINT('Origin',(111.2,23.2,63.));
#105551=CARTESIAN_POINT('',(108.8,23.2,63.));
#105552=CARTESIAN_POINT('Origin',(110.,23.2,63.));
#105553=CARTESIAN_POINT('Origin',(110.,23.05,63.));
#105554=CARTESIAN_POINT('',(108.65,23.05,63.));
#105555=CARTESIAN_POINT('Origin',(110.,21.8,63.));
#105556=CARTESIAN_POINT('Origin',(110.,20.6635,63.));
#105557=CARTESIAN_POINT('Origin',(110.,20.45,63.));
#105558=CARTESIAN_POINT('',(109.,20.2,63.));
#105559=CARTESIAN_POINT('Origin',(110.,20.2,63.));
#105560=CARTESIAN_POINT('',(108.75,20.45,63.));
#105561=CARTESIAN_POINT('Origin',(110.,20.2,63.));
#113957=UNCERTAINTY_MEASURE_WITH_UNIT(LENGTH_MEASURE(0.01),#113985,
'DISTANCE_ACCURACY_VALUE',
'Maximum model space distance between geometric entities at asserted c
onnectivities');
#113964=UNCERTAINTY_MEASURE_WITH_UNIT(LENGTH_MEASURE(0.01),#113985,
'DISTANCE_ACCURACY_VALUE',
'Maximum model space distance between geometric entities at asserted c
onnectivities');
#113977=(
GEOMETRIC_REPRESENTATION_CONTEXT(3)
GLOBAL_UNCERTAINTY_ASSIGNED_CONTEXT((#113957))
GLOBAL_UNIT_ASSIGNED_CONTEXT((#113985,#113987,#113988))
REPRESENTATION_CONTEXT('','3D')
);
#113984=(
GEOMETRIC_REPRESENTATION_CONTEXT(3)
GLOBAL_UNCERTAINTY_ASSIGNED_CONTEXT((#113964))
GLOBAL_UNIT_ASSIGNED_CONTEXT((#113985,#113987,#113988))
REPRESENTATION_CONTEXT('','3D')
);
#113985=(
LENGTH_UNIT()
NAMED_UNIT(*)
SI_UNIT(.MILLI.,.METRE.)
);
#113987=(
NAMED_UNIT(*)
PLANE_ANGLE_UNIT()
SI_UNIT($,.RADIAN.)
);
#113988=(
NAMED_UNIT(*)
SI_UNIT($,.STERADIAN.)
SOLID_ANGLE_UNIT()
);
#114001=SHAPE_DEFINITION_REPRESENTATION(#114020,#114063);
#114020=PRODUCT_DEFINITION_SHAPE('',$,#114083);
#114063=SHAPE_REPRESENTATION('',(#63115),#113977);
#114070=PRODUCT_DEFINITION_CONTEXT('part definition',#114129,'design');
#114083=PRODUCT_DEFINITION('2026-10-05-09-51-47-617',
'ISO 4026 - M3 x 3 - 45H (Knob Set Screw)',#114102,#114070);
#114102=PRODUCT_DEFINITION_FORMATION('',$,#114143);
#114129=APPLICATION_CONTEXT(
'Core Data for Automotive Mechanical Design Process');
#114130=PRODUCT_CONTEXT('part definition',#114129,'mechanical');
#114143=PRODUCT('2026-10-05-09-51-47-617',
'ISO 4026 - M3 x 3 - 45H (Knob Set Screw)',$,(#114130));
#114311=COLOUR_RGB('Black',0.12,0.14,0.17);
#114312=FILL_AREA_STYLE_COLOUR('',#114311);
#114313=FILL_AREA_STYLE('',(#114312));
#114314=SURFACE_STYLE_FILL_AREA(#114313);
#114315=SURFACE_SIDE_STYLE('',(#114314));
#114316=SURFACE_STYLE_USAGE(.BOTH.,#114315);
#114317=PRESENTATION_STYLE_ASSIGNMENT((#114316));
ENDSEC;
END-ISO-10303-21;
